ISO-10303-21;
HEADER;
FILE_DESCRIPTION (('STEP AP214'),
    '1' );
FILE_NAME ('Rotating Grip.step',
    '2026-10-24T00:09:50',
    ( '' ),
    ( '' ),
    'SwSTEP 2.0',
    'SolidWorks 2025',
    '' );
FILE_SCHEMA (( 'AUTOMOTIVE_DESIGN' ));
ENDSEC;

DATA;
#12=EDGE_CURVE ( 'NONE', #4946, #18655, #10877, .T. ) ;
#17=DIRECTION ( 'NONE',  ( 6.123233995736816572E-17, 1.060575238724904203E-16, -1.000000000000000000 ) ) ;
#26=CARTESIAN_POINT ( 'NONE',  ( 160.9807621135329612, 204.9999999999998863, -151.0000000000000284 ) ) ;
#46=PLANE ( 'NONE',  #15936 ) ;
#51=LINE ( 'NONE', #15297, #1051 ) ;
#59=DIRECTION ( 'NONE',  ( -0.000000000000000000, -0.000000000000000000, -1.000000000000000000 ) ) ;
#82=SPHERICAL_SURFACE ( 'NONE', #4853, 35.18636678425505693 ) ;
#95=STYLED_ITEM('',(#28448),#8854);
#108=CARTESIAN_POINT ( 'NONE',  ( 107.6462301271458841, 207.6792144784505467, -139.8040206391607398 ) ) ;
#113=CARTESIAN_POINT ( 'NONE',  ( 338.9795809418241106, 102.2323340340494724, -145.0000000000000000 ) ) ;
#144=AXIS2_PLACEMENT_3D ( 'NONE', #11987, #2630, #13865 ) ;
#166=CARTESIAN_POINT ( 'NONE',  ( 158.4246112489018401, 201.2552156260056222, -141.0358260266776540 ) ) ;
#168=ADVANCED_FACE ( 'NONE', ( #27523 ), #5563, .T. ) ;
#178=EDGE_LOOP ( 'NONE', ( #23936, #17457 ) ) ;
#201=SHAPE_REPRESENTATION ( 'Rotating Grip', ( #10637 ), #10190 ) ;
#212=VERTEX_POINT ( 'NONE', #12332 ) ;
#241=DIRECTION ( 'NONE',  ( -0.8660254037844362651, 0.5000000000000039968, -0.000000000000000000 ) ) ;
#246=DIRECTION ( 'NONE',  ( 0.8660254037844432595, 0.4999999999999919509, -0.000000000000000000 ) ) ;
#254=FACE_OUTER_BOUND ( 'NONE', #27282, .T. ) ;
#256=CARTESIAN_POINT ( 'NONE',  ( 107.3811808525395151, 208.2821736267427752, -140.2307156351394610 ) ) ;
#286=AXIS2_PLACEMENT_3D ( 'NONE', #20944, #11920, #18789 ) ;
#309=ORIENTED_EDGE ( 'NONE', *, *, #678, .T. ) ;
#316=CARTESIAN_POINT ( 'NONE',  ( 134.9999999999998579, 220.0000000000000284, -122.9999999999999574 ) ) ;
#325=EDGE_LOOP ( 'NONE', ( #25386, #12742, #27550, #6157 ) ) ;
#348=DIRECTION ( 'NONE',  ( -0.000000000000000000, -1.000000000000000000, -0.000000000000000000 ) ) ;
#352=CARTESIAN_POINT ( 'NONE',  ( 343.6424681707624700, 87.16319020290713127, -145.0000000000000000 ) ) ;
#370=ORIENTED_EDGE ( 'NONE', *, *, #13729, .T. ) ;
#398=CARTESIAN_POINT ( 'NONE',  ( 106.7495716636776137, 209.9043484200207388, -142.3407963099403446 ) ) ;
#409=ORIENTED_EDGE ( 'NONE', *, *, #12, .F. ) ;
#452=DIRECTION ( 'NONE',  ( -0.000000000000000000, -1.000000000000000000, -0.000000000000000000 ) ) ;
#457=CARTESIAN_POINT ( 'NONE',  ( 319.9779125536060178, 113.2029523930392969, -145.0000000000000000 ) ) ;
#505=CARTESIAN_POINT ( 'NONE',  ( 135.3975132654479125, 250.0000000000000568, -151.0000000000000568 ) ) ;
#519=ORIENTED_EDGE ( 'NONE', *, *, #2998, .T. ) ;
#525=CARTESIAN_POINT ( 'NONE',  ( 113.4538925329242574, 207.5603490538955782, -145.0000000000000000 ) ) ;
#603=CARTESIAN_POINT ( 'NONE',  ( 134.9999999999998579, 220.0000000000000284, -119.9999999999999858 ) ) ;
#613=AXIS2_PLACEMENT_3D ( 'NONE', #4215, #27908, #25767 ) ;
#637=DIRECTION ( 'NONE',  ( -0.000000000000000000, -0.000000000000000000, 1.000000000000000000 ) ) ;
#640=CARTESIAN_POINT ( 'NONE',  ( 162.1315766072936242, 207.1972522101084735, -139.5322470298331439 ) ) ;
#651=CARTESIAN_POINT ( 'NONE',  ( 138.1747091788253954, 249.8319942030928758, -139.9049692442122534 ) ) ;
#678=EDGE_CURVE ( 'NONE', #16059, #28280, #20119, .T. ) ;
#680=DIRECTION ( 'NONE',  ( 0.000000000000000000, 0.000000000000000000, -1.000000000000000000 ) ) ;
#709=CARTESIAN_POINT ( 'NONE',  ( 134.6079681791958365, 250.0000000000001137, -138.9999999999999716 ) ) ;
#751=DIRECTION ( 'NONE',  ( -1.000000000000000000, 0.000000000000000000, -0.000000000000000000 ) ) ;
#772=DIRECTION ( 'NONE',  ( 1.000000000000000000, 0.000000000000000000, 0.000000000000000000 ) ) ;
#789=CARTESIAN_POINT ( 'NONE',  ( 134.9999999999998863, 250.0000000000000568, -151.0000000000000284 ) ) ;
#852=DIRECTION ( 'NONE',  ( 0.000000000000000000, 0.000000000000000000, -1.000000000000000000 ) ) ;
#864=FACE_BOUND ( 'NONE', #3431, .T. ) ;
#870=DIRECTION ( 'NONE',  ( 0.000000000000000000, 0.000000000000000000, -1.000000000000000000 ) ) ;
#875=DIRECTION ( 'NONE',  ( -1.000000000000000000, 0.000000000000000000, 0.000000000000000000 ) ) ;
#878=AXIS2_PLACEMENT_3D ( 'NONE', #9764, #20527, #852 ) ;
#893=CARTESIAN_POINT ( 'NONE',  ( 349.0018770490533484, 96.44595867864246941, -145.0000000000000000 ) ) ;
#911=LINE ( 'NONE', #2923, #8654 ) ;
#914=CARTESIAN_POINT ( 'NONE',  ( 162.2068797070720905, 207.3581635649740917, -139.6159404653925549 ) ) ;
#925=AXIS2_PLACEMENT_3D ( 'NONE', #9640, #25275, #15970 ) ;
#1017=CARTESIAN_POINT ( 'NONE',  ( 110.0398043607047640, 203.3530833388224153, -139.3076717160242595 ) ) ;
#1051=VECTOR ( 'NONE', #4355, 999.9999999999998863 ) ;
#1070=VERTEX_POINT ( 'NONE', #26265 ) ;
#1080=ORIENTED_EDGE ( 'NONE', *, *, #17394, .F. ) ;
#1120=DIRECTION ( 'NONE',  ( -0.000000000000000000, -1.000000000000000000, -0.000000000000000000 ) ) ;
#1131=DIRECTION ( 'NONE',  ( 0.000000000000000000, 0.000000000000000000, -1.000000000000000000 ) ) ;
#1157=CARTESIAN_POINT ( 'NONE',  ( 112.5442897163041636, 200.1067580395811092, -145.3931298709317446 ) ) ;
#1170=ORIENTED_EDGE ( 'NONE', *, *, #1303, .T. ) ;
#1202=APPLICATION_CONTEXT ( 'automotive_design' ) ;
#1235=VERTEX_POINT ( 'NONE', #5848 ) ;
#1242=VERTEX_POINT ( 'NONE', #7866 ) ;
#1284=EDGE_CURVE ( 'NONE', #4946, #19844, #24296, .T. ) ;
#1297=CARTESIAN_POINT ( 'NONE',  ( 112.5172067284654815, 200.1372175834411280, -144.2074248490017681 ) ) ;
#1303=EDGE_CURVE ( 'NONE', #26295, #13229, #18628, .T. ) ;
#1310=ORIENTED_EDGE ( 'NONE', *, *, #17394, .T. ) ;
#1332=CARTESIAN_POINT ( 'NONE',  ( 162.8938219812283137, 208.9567185848077600, -149.1019530262190642 ) ) ;
#1375=CARTESIAN_POINT ( 'NONE',  ( 134.9999999999998295, 537.6859242279716682, -683.1631314933625845 ) ) ;
#1378=EDGE_CURVE ( 'NONE', #1070, #21067, #12185, .T. ) ;
#1403=CARTESIAN_POINT ( 'NONE',  ( 129.2024882373296464, 249.4345418698963215, -143.4419542882358485 ) ) ;
#1407=LINE ( 'NONE', #16509, #23066 ) ;
#1414=EDGE_CURVE ( 'NONE', #8004, #24318, #9874, .T. ) ;
#1433=CARTESIAN_POINT ( 'NONE',  ( 110.3467068720617590, 202.9047393083059205, -139.5322470298331439 ) ) ;
#1471=CARTESIAN_POINT ( 'NONE',  ( 163.1912130698789554, 209.7382084964983733, -148.0040471605078380 ) ) ;
#1488=CIRCLE ( 'NONE', #16191, 10.71881775658151170 ) ;
#1513=DIRECTION ( 'NONE',  ( -0.000000000000000000, -0.000000000000000000, 1.000000000000000000 ) ) ;
#1528=VERTEX_POINT ( 'NONE', #24940 ) ;
#1556=CARTESIAN_POINT ( 'NONE',  ( 106.6702556437889484, 210.1292660578155562, -147.1195141158910360 ) ) ;
#1580=CARTESIAN_POINT ( 'NONE',  ( -68.97958094182604327, 102.2323340340523288, -162.9307281190808681 ) ) ;
#1610=CARTESIAN_POINT ( 'NONE',  ( 163.4054721189930035, 210.3495760014581606, -143.6319245046324511 ) ) ;
#1611=ORIENTED_EDGE ( 'NONE', *, *, #3192, .T. ) ;
#1623=DIRECTION ( 'NONE',  ( 0.000000000000000000, 0.000000000000000000, -1.000000000000000000 ) ) ;
#1656=CARTESIAN_POINT ( 'NONE',  ( 134.9999999999998579, 220.0000000000000284, 109.9999999999999858 ) ) ;
#1664=LINE ( 'NONE', #21342, #1954 ) ;
#1676=DIRECTION ( 'NONE',  ( 0.8660254037844432595, 0.4999999999999919509, -0.000000000000000000 ) ) ;
#1686=CARTESIAN_POINT ( 'NONE',  ( -20.92338318254765994, 120.7399884395670142, -145.0000000000000000 ) ) ;
#1692=CARTESIAN_POINT ( 'NONE',  ( 108.3633886251205638, 206.1968162351656986, -150.8460904732142183 ) ) ;
#1722=EDGE_CURVE ( 'NONE', #9931, #11276, #6796, .T. ) ;
#1746=ORIENTED_EDGE ( 'NONE', *, *, #15857, .T. ) ;
#1772=EDGE_LOOP ( 'NONE', ( #25202, #14510, #24999, #3530, #23753 ) ) ;
#1820=CARTESIAN_POINT ( 'NONE',  ( 128.9998022404941480, 249.3938365459133593, -145.3931298709317446 ) ) ;
#1846=ADVANCED_FACE ( 'NONE', ( #17434 ), #21604, .T. ) ;
#1877=VERTEX_POINT ( 'NONE', #15723 ) ;
#1884=CARTESIAN_POINT ( 'NONE',  ( 158.0554390835131642, 200.8047184523794897, -141.8266621613457232 ) ) ;
#1899=SHAPE_REPRESENTATION_RELATIONSHIP ( 'NONE' , 'NONE' ,  #201, #25288 ) ;
#1920=CARTESIAN_POINT ( 'NONE',  ( -79.00187704905530950, 96.44595867864546790, -145.0000000000000000 ) ) ;
#1954=VECTOR ( 'NONE', #23788, 999.9999999999998863 ) ;
#1955=DIRECTION ( 'NONE',  ( -0.5000000000000039968, -0.8660254037844362651, -1.224646799147353454E-16 ) ) ;
#1962=CARTESIAN_POINT ( 'NONE',  ( 133.0594107791237661, 249.9377649212624419, -150.6809294437986182 ) ) ;
#1972=CARTESIAN_POINT ( 'NONE',  ( 107.7878109108858098, 207.3655475159964681, -150.3903514073973611 ) ) ;
#2013=EDGE_CURVE ( 'NONE', #23466, #21067, #4383, .T. ) ;
#2032=CARTESIAN_POINT ( 'NONE',  ( 160.5791959497488222, 204.3237910346065291, -139.0484678162420380 ) ) ;
#2058=ORIENTED_EDGE ( 'NONE', *, *, #23518, .T. ) ;
#2062=FACE_OUTER_BOUND ( 'NONE', #20613, .T. ) ;
#2065=DIRECTION ( 'NONE',  ( 1.000000000000000000, 0.000000000000000000, 0.000000000000000000 ) ) ;
#2076=DIRECTION ( 'NONE',  ( -1.000000000000000000, 0.000000000000000000, 0.000000000000000000 ) ) ;
#2114=FACE_BOUND ( 'NONE', #9534, .T. ) ;
#2136=CARTESIAN_POINT ( 'NONE',  ( 134.9999999999998579, 404.6636166603179277, -145.0000000000000000 ) ) ;
#2171=DIRECTION ( 'NONE',  ( -0.4999999999999919509, 0.8660254037844432595, -1.224646799147353207E-16 ) ) ;
#2194=CARTESIAN_POINT ( 'NONE',  ( 113.4538925329242574, 207.5603490538955782, -145.0000000000000000 ) ) ;
#2196=DIRECTION ( 'NONE',  ( 0.000000000000000000, 0.000000000000000000, -1.000000000000000000 ) ) ;
#2204=CARTESIAN_POINT ( 'NONE',  ( 134.9999999999998863, 404.6636166603179277, -137.0000000000000000 ) ) ;
#2257=ORIENTED_EDGE ( 'NONE', *, *, #11814, .T. ) ;
#2304=CARTESIAN_POINT ( 'NONE',  ( 157.4557401840683610, 200.1067917919123431, -144.6099047286053576 ) ) ;
#2320=DIRECTION ( 'NONE',  ( 0.000000000000000000, 0.000000000000000000, 1.000000000000000000 ) ) ;
#2322=EDGE_CURVE ( 'NONE', #20571, #1242, #24589, .T. ) ;
#2336=DIRECTION ( 'NONE',  ( 0.8660254037844432595, 0.4999999999999919509, -0.000000000000000000 ) ) ;
#2354=CARTESIAN_POINT ( 'NONE',  ( 138.9677719900889770, 249.7377618559918062, -149.5176478624189542 ) ) ;
#2355=ORIENTED_EDGE ( 'NONE', *, *, #20263, .F. ) ;
#2390=CARTESIAN_POINT ( 'NONE',  ( 108.9212046047250055, 205.1697986248093173, -138.9999999999999432 ) ) ;
#2425=ORIENTED_EDGE ( 'NONE', *, *, #7125, .F. ) ;
#2449=CARTESIAN_POINT ( 'NONE',  ( 157.4819278492304875, 200.1362360204147137, -145.7848141779618629 ) ) ;
#2497=CARTESIAN_POINT ( 'NONE',  ( 140.0958819112771891, 249.5642367155375041, -141.8266621613457801 ) ) ;
#2630=DIRECTION ( 'NONE',  ( -0.8660254037844362651, 0.5000000000000039968, -0.000000000000000000 ) ) ;
#2646=CARTESIAN_POINT ( 'NONE',  ( 138.6614742573536887, 249.7775121908574079, -140.2307156351394895 ) ) ;
#2664=APPLICATION_CONTEXT ( 'automotive_design' ) ;
#2680=CIRCLE ( 'NONE', #25623, 10.71881775658151170 ) ;
#2753=EDGE_LOOP ( 'NONE', ( #26641, #12361, #6078, #23797 ) ) ;
#2770=AXIS2_PLACEMENT_3D ( 'NONE', #28338, #15160, #19734 ) ;
#2788=CARTESIAN_POINT ( 'NONE',  ( 140.4672727784185327, 249.4977086558912731, -142.5205423047663373 ) ) ;
#2796=CARTESIAN_POINT ( 'NONE',  ( 161.9999999999998863, 220.0000000000000284, -119.9999999999999858 ) ) ;
#2803=AXIS2_PLACEMENT_3D ( 'NONE', #20977, #25146, #18683 ) ;
#2805=ORIENTED_EDGE ( 'NONE', *, *, #13521, .F. ) ;
#2841=TOROIDAL_SURFACE ( 'NONE', #3301, -538.1631314933625845, 562.1290781602207289 ) ;
#2878=ADVANCED_FACE ( 'NONE', ( #19315 ), #28058, .T. ) ;
#2887=DIRECTION ( 'NONE',  ( 0.000000000000000000, 0.000000000000000000, -1.000000000000000000 ) ) ;
#2923=CARTESIAN_POINT ( 'NONE',  ( 164.9999999999998579, 220.0000000000000284, -169.9999999999999716 ) ) ;
#2952=ORIENTED_EDGE ( 'NONE', *, *, #3192, .F. ) ;
#2973=VERTEX_POINT ( 'NONE', #15730 ) ;
#2998=EDGE_CURVE ( 'NONE', #23714, #1235, #14208, .T. ) ;
#3032=EDGE_CURVE ( 'NONE', #212, #5309, #5919, .T. ) ;
#3034=DIRECTION ( 'NONE',  ( -0.000000000000000000, -1.000000000000000000, -0.000000000000000000 ) ) ;
#3055=CARTESIAN_POINT ( 'NONE',  ( 338.9795809418241106, 102.2323340340494298, -162.9307281190808681 ) ) ;
#3059=CARTESIAN_POINT ( 'NONE',  ( 161.3653042226020204, 205.6814106928004833, -139.0380470571626574 ) ) ;
#3110=ORIENTED_EDGE ( 'NONE', *, *, #9960, .F. ) ;
#3117=EDGE_CURVE ( 'NONE', #15076, #1070, #10707, .T. ) ;
#3122=CARTESIAN_POINT ( 'NONE',  ( 338.9795809418241106, 102.2323340340494155, -127.0692718809191035 ) ) ;
#3155=EDGE_CURVE ( 'NONE', #17557, #4843, #5663, .T. ) ;
#3192=EDGE_CURVE ( 'NONE', #17930, #19026, #5511, .T. ) ;
#3212=CARTESIAN_POINT ( 'NONE',  ( 135.9832230577667360, 249.9845044293635965, -139.0778438077165333 ) ) ;
#3222=VERTEX_POINT ( 'NONE', #20681 ) ;
#3228=EDGE_CURVE ( 'NONE', #13771, #11671, #5962, .T. ) ;
#3271=ORIENTED_EDGE ( 'NONE', *, *, #14791, .T. ) ;
#3289=ORIENTED_EDGE ( 'NONE', *, *, #9470, .F. ) ;
#3301=AXIS2_PLACEMENT_3D ( 'NONE', #14465, #10717, #16760 ) ;
#3338=CARTESIAN_POINT ( 'NONE',  ( 163.4559080432011058, 210.4994054145057021, -145.3931298709317730 ) ) ;
#3373=CARTESIAN_POINT ( 'NONE',  ( 134.9999999999998579, 455.5353319318992362, -145.0000000000000000 ) ) ;
#3412=CARTESIAN_POINT ( 'NONE',  ( -24.92338318254761020, 127.6681916698425567, -151.0000000000000284 ) ) ;
#3431=EDGE_LOOP ( 'NONE', ( #15629, #17894 ) ) ;
#3436=CONICAL_SURFACE ( 'NONE', #8040, 30.00000000000001421, 0.4537856055185259252 ) ;
#3445=CARTESIAN_POINT ( 'NONE',  ( 109.8358256782556452, 203.6659868461599388, -150.7960377432351606 ) ) ;
#3449=ORIENTED_EDGE ( 'NONE', *, *, #25330, .F. ) ;
#3456=AXIS2_PLACEMENT_3D ( 'NONE', #9996, #8404, #21608 ) ;
#3483=CARTESIAN_POINT ( 'NONE',  ( 163.3519221325304898, 210.1932722521781045, -143.0657854549350532 ) ) ;
#3494=DIRECTION ( 'NONE',  ( -0.000000000000000000, -1.000000000000000000, -0.000000000000000000 ) ) ;
#3527=FACE_OUTER_BOUND ( 'NONE', #22907, .T. ) ;
#3530=ORIENTED_EDGE ( 'NONE', *, *, #23525, .T. ) ;
#3550=CARTESIAN_POINT ( 'NONE',  ( 130.2364926426604086, 249.6196707243893229, -148.6534330424975678 ) ) ;
#3583=CARTESIAN_POINT ( 'NONE',  ( 109.8320145249364259, 203.6683199386712602, -139.1927212198768586 ) ) ;
#3595=EDGE_LOOP ( 'NONE', ( #18286, #18778, #13663, #19227, #11134 ) ) ;
#3618=CARTESIAN_POINT ( 'NONE',  ( 162.9423453941602702, 209.0802367224323746, -148.9571385985324810 ) ) ;
#3635=CARTESIAN_POINT ( 'NONE',  ( 349.0018770490533484, 96.44595867864246941, -145.0000000000000000 ) ) ;
#3679=AXIS2_PLACEMENT_3D ( 'NONE', #7678, #3494, #18866 ) ;
#3700=CARTESIAN_POINT ( 'NONE',  ( 106.6482032540381510, 210.1929095456142704, -146.9353207969096786 ) ) ;
#3724=CARTESIAN_POINT ( 'NONE',  ( 112.0174213346884926, 200.7165890697358464, -148.0040471605077812 ) ) ;
#3726=CARTESIAN_POINT ( 'NONE',  ( 294.9233831825459902, 127.6681916698402830, -137.0000000000000000 ) ) ;
#3737=EDGE_CURVE ( 'NONE', #18655, #20571, #2680, .T. ) ;
#3770=AXIS2_PLACEMENT_3D ( 'NONE', #12055, #1120, #23102 ) ;
#3800=EDGE_CURVE ( 'NONE', #11671, #11276, #911, .T. ) ;
#3815=VERTEX_POINT ( 'NONE', #18013 ) ;
#3822=AXIS2_PLACEMENT_3D ( 'NONE', #10599, #3844, #27959 ) ;
#3839=CARTESIAN_POINT ( 'NONE',  ( 132.3447116496838305, 249.8827672015449082, -139.6159404653925833 ) ) ;
#3844=DIRECTION ( 'NONE',  ( -0.000000000000000000, -0.000000000000000000, 1.000000000000000000 ) ) ;
#3856=ORIENTED_EDGE ( 'NONE', *, *, #11443, .F. ) ;
#3934=CIRCLE ( 'NONE', #19994, 10.71881775658151170 ) ;
#3957=ORIENTED_EDGE ( 'NONE', *, *, #3032, .T. ) ;
#3975=CARTESIAN_POINT ( 'NONE',  ( 130.2301963871595945, 249.6192082491895974, -141.3391815462162810 ) ) ;
#4025=ADVANCED_FACE ( 'NONE', ( #8221 ), #6060, .T. ) ;
#4027=ORIENTED_EDGE ( 'NONE', *, *, #3800, .T. ) ;
#4046=PLANE ( 'NONE',  #17510 ) ;
#4059=AXIS2_PLACEMENT_3D ( 'NONE', #21864, #2171, #10948 ) ;
#4077=EDGE_CURVE ( 'NONE', #4843, #17557, #17612, .T. ) ;
#4118=CARTESIAN_POINT ( 'NONE',  ( 131.9979426672184672, 249.8499243485765646, -139.8013169873307788 ) ) ;
#4129=CARTESIAN_POINT ( 'NONE',  ( -140.1240808061633345, 61.15703788601678781, -145.0000000000000000 ) ) ;
#4152=CARTESIAN_POINT ( 'NONE',  ( 109.0192378864665557, 205.0000000000002842, -151.0000000000000284 ) ) ;
#4198=( LENGTH_UNIT ( ) NAMED_UNIT ( * ) SI_UNIT ( .MILLI., .METRE. ) );
#4215=CARTESIAN_POINT ( 'NONE',  ( 134.9999999999998579, 457.0747856552986832, -145.0000000000000000 ) ) ;
#4276=CARTESIAN_POINT ( 'NONE',  ( 106.5565118542854322, 210.4619613463102894, -145.7848141779619198 ) ) ;
#4295=UNCERTAINTY_MEASURE_WITH_UNIT (LENGTH_MEASURE( 1.000000000000000082E-05 ), #4198, 'distance_accuracy_value', 'NONE');
#4327=CARTESIAN_POINT ( 'NONE',  ( 159.3470388241378259, 202.4691944533894912, -150.2059422892478722 ) ) ;
#4350=DIRECTION ( 'NONE',  ( 1.000000000000000000, 0.000000000000000000, -0.000000000000000000 ) ) ;
#4355=DIRECTION ( 'NONE',  ( -0.8660254037844363761, 0.5000000000000039968, -0.000000000000000000 ) ) ;
#4358=DIRECTION ( 'NONE',  ( -0.000000000000000000, -0.000000000000000000, -1.000000000000000000 ) ) ;
#4383=CIRCLE ( 'NONE', #11759, 17.93072811908088937 ) ;
#4411=CARTESIAN_POINT ( 'NONE',  ( -68.97958094182604327, 102.2323340340523288, -145.0000000000000000 ) ) ;
#4414=EDGE_CURVE ( 'NONE', #21067, #8004, #9544, .T. ) ;
#4422=CARTESIAN_POINT ( 'NONE',  ( 134.9999999999998579, 467.1080826427131001, -145.0000000000000000 ) ) ;
#4474=ORIENTED_EDGE ( 'NONE', *, *, #21612, .F. ) ;
#4550=CARTESIAN_POINT ( 'NONE',  ( 108.2714812867982488, 206.3715290211474382, -139.1934629298939683 ) ) ;
#4589=ORIENTED_EDGE ( 'NONE', *, *, #3228, .F. ) ;
#4604=CARTESIAN_POINT ( 'NONE',  ( 160.7820054808089196, 204.6557434137805274, -151.0000000000000568 ) ) ;
#4614=ADVANCED_FACE ( 'NONE', ( #11787 ), #17789, .T. ) ;
#4629=EDGE_CURVE ( 'NONE', #1528, #3222, #19165, .T. ) ;
#4649=DIRECTION ( 'NONE',  ( -0.000000000000000000, -1.000000000000000000, -0.000000000000000000 ) ) ;
#4651=CARTESIAN_POINT ( 'NONE',  ( 140.1965873975519230, 249.5466472113101872, -141.9943226514402568 ) ) ;
#4691=AXIS2_PLACEMENT_3D ( 'NONE', #9033, #15649, #22243 ) ;
#4699=CIRCLE ( 'NONE', #18477, 10.71881775658151170 ) ;
#4726=B_SPLINE_CURVE_WITH_KNOTS ( 'NONE', 3,
 ( #14384, #9791, #18965, #3583, #1017, #1433, #7906, #8186, #18547, #16400, #12096, #27709, #16953, #8047, #25706, #16538, #16815, #25561, #6029, #1297, #14810, #1157, #5465, #23140, #27293, #23415, #3724, #7633, #12515, #23561, #11951, #25145, #14247, #18682, #20693, #22996, #25287, #3445, #21836, #8759, #26134, #4152 ),
 .UNSPECIFIED., .F., .F.,
 ( 4, 2, 2, 2, 2, 2, 2, 2, 2, 2, 2, 2, 2, 2, 2, 2, 2, 2, 2, 2, 4 ),
 ( 0.01880622955133634880, 0.01998131524074750476, 0.02115640093015866419, 0.02174394377486424737, 0.02233148661956983055, 0.02350657230898089631, 0.02468165799839196206, 0.02585674368780302781, 0.02644428653250854855, 0.02703182937721406581, 0.02820691506662520789, 0.02938200075603634651, 0.03055708644544748859, 0.03173217213485862720, 0.03231971497956417916, 0.03290725782426972418, 0.03408234351368071013, 0.03525742920309170303, 0.03584497204779715784, 0.03643251489250261960, 0.03760760058191347371 ),
 .UNSPECIFIED. ) ;
#4765=ORIENTED_EDGE ( 'NONE', *, *, #15857, .F. ) ;
#4800=CARTESIAN_POINT ( 'NONE',  ( 138.6601105629808899, 249.7776935521190182, -149.7704424372629717 ) ) ;
#4806=ORIENTED_EDGE ( 'NONE', *, *, #3032, .F. ) ;
#4818=CARTESIAN_POINT ( 'NONE',  ( 294.9233831825460470, 127.6681916698403398, -145.0000000000000000 ) ) ;
#4829=CARTESIAN_POINT ( 'NONE',  ( 164.9999999999998579, 220.0000000000000284, -169.9999999999999716 ) ) ;
#4843=VERTEX_POINT ( 'NONE', #21506 ) ;
#4853=AXIS2_PLACEMENT_3D ( 'NONE', #28080, #21779, #19479 ) ;
#4928=ORIENTED_EDGE ( 'NONE', *, *, #26599, .F. ) ;
#4934=ORIENTED_EDGE ( 'NONE', *, *, #23793, .F. ) ;
#4939=CARTESIAN_POINT ( 'NONE',  ( 140.2062392899099734, 249.5456347581138914, -148.0084258618598767 ) ) ;
#4946=VERTEX_POINT ( 'NONE', #14919 ) ;
#4950=EDGE_LOOP ( 'NONE', ( #2805, #16799 ) ) ;
#4957=EDGE_CURVE ( 'NONE', #3222, #23714, #14164, .T. ) ;
#4969=DIRECTION ( 'NONE',  ( 0.000000000000000000, 0.000000000000000000, -1.000000000000000000 ) ) ;
#5006=CARTESIAN_POINT ( 'NONE',  ( 340.3127869742386338, 101.4626071723496779, -145.0000000000000000 ) ) ;
#5023=CARTESIAN_POINT ( 'NONE',  ( 298.9233831825461039, 134.5963949001157687, -145.0000000000000000 ) ) ;
#5024=DIRECTION ( 'NONE',  ( -0.000000000000000000, -0.000000000000000000, 1.000000000000000000 ) ) ;
#5038=FACE_OUTER_BOUND ( 'NONE', #8347, .T. ) ;
#5088=CARTESIAN_POINT ( 'NONE',  ( 138.0086035401004665, 249.8505569019347661, -150.2059422892478153 ) ) ;
#5133=ADVANCED_FACE ( 'NONE', ( #27364 ), #11411, .T. ) ;
#5144=UNCERTAINTY_MEASURE_WITH_UNIT (LENGTH_MEASURE( 1.000000000000000082E-05 ), #26485, 'distance_accuracy_value', 'NONE');
#5149=DIRECTION ( 'NONE',  ( 0.000000000000000000, 0.000000000000000000, -1.000000000000000000 ) ) ;
#5158=FACE_OUTER_BOUND ( 'NONE', #325, .T. ) ;
#5164=EDGE_CURVE ( 'NONE', #1242, #19224, #19661, .T. ) ;
#5188=FACE_OUTER_BOUND ( 'NONE', #28258, .T. ) ;
#5233=CARTESIAN_POINT ( 'NONE',  ( 135.3925546936119417, 249.9980781680236532, -139.0095862629495116 ) ) ;
#5282=AXIS2_PLACEMENT_3D ( 'NONE', #26032, #21735, #16860 ) ;
#5296=DIRECTION ( 'NONE',  ( -0.8660254037844363761, 0.5000000000000041078, -0.000000000000000000 ) ) ;
#5309=VERTEX_POINT ( 'NONE', #12871 ) ;
#5315=EDGE_LOOP ( 'NONE', ( #25611, #3271, #28290, #4765 ) ) ;
#5340=B_SPLINE_CURVE_WITH_KNOTS ( 'NONE', 3,
 ( #789, #505, #24491, #24341, #9557, #13300, #13877, #22336, #5088, #4800, #2354, #22630, #9268, #4939, #13439, #22193, #11137, #9120, #26482, #17735, #6956, #9416, #11579, #6813, #13733, #2788, #15598, #4651, #2497, #11287, #26633, #13587, #2646, #651, #20177, #26788, #18177, #26931, #7679, #3212, #10118, #5233, #20739, #11998 ),
 .UNSPECIFIED., .F., .F.,
 ( 4, 2, 2, 2, 2, 2, 2, 2, 2, 2, 2, 2, 2, 2, 2, 2, 2, 2, 2, 2, 2, 4 ),
 ( 2.775557561562891351E-17, 0.001175389346958573842, 0.001763084020437806227, 0.002350778693917038829, 0.003526168040875585132, 0.004701557387834132302, 0.005876946734792679039, 0.007052336081751224908, 0.007640030755230537741, 0.008227725428709848840, 0.009403114775668379097, 0.01057850412262690762, 0.01175389346958543614, 0.01234158814306466484, 0.01292928281654389007, 0.01410467216350234400, 0.01528006151046080140, 0.01586775618394002663, 0.01645545085741925359, 0.01763084020437779079, 0.01821853487785705938, 0.01880622955133632798 ),
 .UNSPECIFIED. ) ;
#5358=EDGE_CURVE ( 'NONE', #1242, #19844, #20581, .T. ) ;
#5394=EDGE_CURVE ( 'NONE', #5589, #15093, #8827, .T. ) ;
#5446=VECTOR ( 'NONE', #14737, 1000.000000000000000 ) ;
#5465=CARTESIAN_POINT ( 'NONE',  ( 112.5180643521146635, 200.1362485301921481, -145.7833319456713639 ) ) ;
#5511=CIRCLE ( 'NONE', #14683, 20.24534822868278994 ) ;
#5515=ORIENTED_EDGE ( 'NONE', *, *, #17984, .T. ) ;
#5531=ORIENTED_EDGE ( 'NONE', *, *, #14454, .T. ) ;
#5563=CYLINDRICAL_SURFACE ( 'NONE', #21882, 6.000000000000032863 ) ;
#5588=VERTEX_POINT ( 'NONE', #1580 ) ;
#5589=VERTEX_POINT ( 'NONE', #19249 ) ;
#5604=PLANE ( 'NONE',  #9875 ) ;
#5622=CIRCLE ( 'NONE', #19853, 27.00000000000002487 ) ;
#5640=CARTESIAN_POINT ( 'NONE',  ( -49.97791255360778706, 113.2029523930418975, -145.0000000000000000 ) ) ;
#5649=CARTESIAN_POINT ( 'NONE',  ( -24.92338318254761020, 127.6681916698425567, -138.9999999999999432 ) ) ;
#5663=B_SPLINE_CURVE_WITH_KNOTS ( 'NONE', 3,
 ( #20306, #20591, #3059, #11419, #20164, #640, #914, #9682, #18442, #27194, #7533, #16295, #9823, #5783, #23172, #14558, #3483, #14280, #1610, #14845, #25593, #3338, #23310, #21150, #16983, #21291, #1471, #12270, #21004, #3618, #1332, #14418, #10102, #10380, #23449, #9958, #12410, #25461, #18856, #25737, #19136, #16711 ),
 .UNSPECIFIED., .F., .F.,
 ( 4, 2, 2, 2, 2, 2, 2, 2, 2, 2, 2, 2, 2, 2, 2, 2, 2, 2, 2, 2, 4 ),
 ( 0.01880622955133633145, 0.01998131524074743884, 0.02115640093015854623, 0.02174394377486411900, 0.02233148661956969178, 0.02350657230898078875, 0.02468165799839188920, 0.02585674368780298965, 0.02644428653250852079, 0.02703182937721405193, 0.02820691506662503442, 0.02938200075603601691, 0.03055708644544699593, 0.03173217213485798188, 0.03231971497956351302, 0.03290725782426905111, 0.03408234351368011339, 0.03525742920309117567, 0.03584497204779672763, 0.03643251489250227265, 0.03760760058191342514 ),
 .UNSPECIFIED. ) ;
#5702=ORIENTED_EDGE ( 'NONE', *, *, #24700, .T. ) ;
#5720=EDGE_CURVE ( 'NONE', #19224, #27008, #11458, .T. ) ;
#5731=EDGE_LOOP ( 'NONE', ( #19825, #19189, #11761, #12156 ) ) ;
#5783=CARTESIAN_POINT ( 'NONE',  ( 163.1896802570002478, 209.7340148635404944, -141.9885977063035227 ) ) ;
#5848=CARTESIAN_POINT ( 'NONE',  ( -79.00187704905532371, 96.44595867864549632, -134.2811822434184137 ) ) ;
#5852=CARTESIAN_POINT ( 'NONE',  ( 129.6073710054587309, 249.5117418702950829, -147.6595947404202320 ) ) ;
#5861=CARTESIAN_POINT ( 'NONE',  ( 106.5567364938767838, 210.4612944616921482, -144.2111520032349006 ) ) ;
#5872=ADVANCED_FACE ( 'NONE', ( #5158 ), #7770, .T. ) ;
#5919=CIRCLE ( 'NONE', #16520, 35.18636678425504982 ) ;
#5921=DIRECTION ( 'NONE',  ( -0.000000000000000000, -1.000000000000000000, -0.000000000000000000 ) ) ;
#5928=ORIENTED_EDGE ( 'NONE', *, *, #21612, .T. ) ;
#5962=CIRCLE ( 'NONE', #925, 30.00000000000001421 ) ;
#5964=CARTESIAN_POINT ( 'NONE',  ( 124.9999999999998579, 220.0000000000000284, -119.9999999999999858 ) ) ;
#5987=FACE_OUTER_BOUND ( 'NONE', #1772, .T. ) ;
#6005=DIRECTION ( 'NONE',  ( 1.000000000000000000, 0.000000000000000000, 0.000000000000000000 ) ) ;
#6029=CARTESIAN_POINT ( 'NONE',  ( 112.4397516004750202, 200.2253515377324788, -143.6319245046325364 ) ) ;
#6060=SPHERICAL_SURFACE ( 'NONE', #12300, 35.18636678425505693 ) ;
#6078=ORIENTED_EDGE ( 'NONE', *, *, #13080, .T. ) ;
#6121=CARTESIAN_POINT ( 'NONE',  ( -49.97791255360778706, 113.2029523930418975, -145.0000000000000000 ) ) ;
#6142=ADVANCED_FACE ( 'NONE', ( #19358 ), #19505, .T. ) ;
#6155=ADVANCED_FACE ( 'NONE', ( #254 ), #17343, .T. ) ;
#6157=ORIENTED_EDGE ( 'NONE', *, *, #5720, .F. ) ;
#6160=ORIENTED_EDGE ( 'NONE', *, *, #13080, .F. ) ;
#6173=CIRCLE ( 'NONE', #22699, 35.18636678425505693 ) ;
#6185=SHAPE_DEFINITION_REPRESENTATION ( #21034, #201 ) ;
#6238=SPHERICAL_SURFACE ( 'NONE', #28229, 35.18636678425505693 ) ;
#6278=CARTESIAN_POINT ( 'NONE',  ( 130.6168512560825832, 249.6783991519806705, -149.1019530262190358 ) ) ;
#6289=ORIENTED_EDGE ( 'NONE', *, *, #5720, .T. ) ;
#6380=DIRECTION ( 'NONE',  ( 0.8660254037844432595, 0.4999999999999919509, -0.000000000000000000 ) ) ;
#6423=FACE_OUTER_BOUND ( 'NONE', #27077, .T. ) ;
#6432=CARTESIAN_POINT ( 'NONE',  ( 107.6443576357609828, 207.6802486446758564, -150.2059422892478722 ) ) ;
#6455=CARTESIAN_POINT ( 'NONE',  ( 410.1240808061609755, 61.15703788601290114, -683.1631314933625845 ) ) ;
#6458=DIRECTION ( 'NONE',  ( 0.000000000000000000, 0.000000000000000000, -1.000000000000000000 ) ) ;
#6484=CARTESIAN_POINT ( 'NONE',  ( -84.36128592734598897, 105.7287271543808487, -145.0000000000000000 ) ) ;
#6485=CARTESIAN_POINT ( 'NONE',  ( 160.5798347354847238, 204.3213570346847519, -150.9608879355640170 ) ) ;
#6499=CARTESIAN_POINT ( 'NONE',  ( -24.92338318254761020, 127.6681916698425567, -145.0000000000000000 ) ) ;
#6522=DIRECTION ( 'NONE',  ( 0.000000000000000000, 0.000000000000000000, -1.000000000000000000 ) ) ;
#6574=CARTESIAN_POINT ( 'NONE',  ( 134.9999999999998579, 220.0000000000000284, -119.9999999999999858 ) ) ;
#6600=DIRECTION ( 'NONE',  ( 0.8660254037844363761, -0.5000000000000039968, 0.000000000000000000 ) ) ;
#6633=CARTESIAN_POINT ( 'NONE',  ( 158.9581838007524084, 201.9414044957390786, -149.7704424372630001 ) ) ;
#6636=CARTESIAN_POINT ( 'NONE',  ( 164.9999999999998579, 220.0000000000000284, -169.9999999999999716 ) ) ;
#6662=DIRECTION ( 'NONE',  ( -1.000000000000000000, 0.000000000000000000, 0.000000000000000000 ) ) ;
#6698=CARTESIAN_POINT ( 'NONE',  ( 160.9807621135329612, 204.9999999999999147, -138.9999999999999432 ) ) ;
#6711=CIRCLE ( 'NONE', #19098, 6.000000000000005329 ) ;
#6752=EDGE_CURVE ( 'NONE', #5309, #4946, #24311, .T. ) ;
#6759=ORIENTED_EDGE ( 'NONE', *, *, #17984, .F. ) ;
#6765=CARTESIAN_POINT ( 'NONE',  ( 159.2479102360155423, 202.3346240999630368, -139.9049692442122534 ) ) ;
#6773=AXIS2_PLACEMENT_3D ( 'NONE', #5006, #5296, #13798 ) ;
#6796=LINE ( 'NONE', #23908, #18604 ) ;
#6813=CARTESIAN_POINT ( 'NONE',  ( 140.8071701735416354, 249.4326844987137974, -143.4408232581956213 ) ) ;
#6917=CARTESIAN_POINT ( 'NONE',  ( 294.9233831825460470, 127.6681916698403398, -145.0000000000000000 ) ) ;
#6932=AXIS2_PLACEMENT_3D ( 'NONE', #1686, #21799, #10454 ) ;
#6956=CARTESIAN_POINT ( 'NONE',  ( 140.9998454966672625, 249.3939084512563511, -145.3948054049556617 ) ) ;
#6981=AXIS2_PLACEMENT_3D ( 'NONE', #17031, #17177, #21340 ) ;
#6996=CARTESIAN_POINT ( 'NONE',  ( 108.8246248949738373, 205.3409232530312636, -139.0095862629494547 ) ) ;
#7007=B_SPLINE_CURVE_WITH_KNOTS ( 'NONE', 3,
 ( #19081, #21376, #21233, #1692, #12914, #21660, #27966, #1972, #6432, #10752, #23964, #27686, #19508, #26104, #14635, #1556, #3700, #28253, #15211, #4276, #21091, #16791, #5861, #18940, #8021, #11323, #398, #9304, #24241, #24672, #13197, #17485, #256, #22085, #108, #26521, #11033, #15354, #4550, #11471, #7145, #6996, #2390, #13061 ),
 .UNSPECIFIED., .F., .F.,
 ( 4, 2, 2, 2, 2, 2, 2, 2, 2, 2, 2, 2, 2, 2, 2, 2, 2, 2, 2, 2, 2, 4 ),
 ( 3.103167691559091397E-17, 0.001175389346958652555, 0.001763084020437963436, 0.002350778693917274318, 0.003526168040875896081, 0.004701557387834517411, 0.005876946734793139608, 0.007052336081751760938, 0.007640030755231059893, 0.008227725428710357114, 0.009403114775668859615, 0.01057850412262736385, 0.01175389346958586462, 0.01234158814306509158, 0.01292928281654431508, 0.01410467216350273084, 0.01528006151046114661, 0.01586775618394034582, 0.01645545085741954502, 0.01763084020437794691, 0.01821853487785714959, 0.01880622955133634880 ),
 .UNSPECIFIED. ) ;
#7125=EDGE_CURVE ( 'NONE', #18109, #11335, #21681, .T. ) ;
#7141=FACE_OUTER_BOUND ( 'NONE', #15182, .T. ) ;
#7145=CARTESIAN_POINT ( 'NONE',  ( 108.6344068260611948, 205.6858709818343982, -139.0484678162420948 ) ) ;
#7157=ORIENTED_EDGE ( 'NONE', *, *, #25981, .T. ) ;
#7215=EDGE_LOOP ( 'NONE', ( #11969, #18305, #8692, #10506 ) ) ;
#7270=AXIS2_PLACEMENT_3D ( 'NONE', #18167, #26920, #12413 ) ;
#7318=CARTESIAN_POINT ( 'NONE',  ( -79.00187704905530950, 96.44595867864546790, -145.0000000000000000 ) ) ;
#7328=VERTEX_POINT ( 'NONE', #22081 ) ;
#7337=CARTESIAN_POINT ( 'NONE',  ( 104.9999999999998579, 220.0000000000000284, -169.9999999999999716 ) ) ;
#7363=CARTESIAN_POINT ( 'NONE',  ( 104.9999999999998579, 220.0000000000000284, -169.9999999999999716 ) ) ;
#7370=VERTEX_POINT ( 'NONE', #5649 ) ;
#7379=ADVANCED_FACE ( 'NONE', ( #7141 ), #26821, .T. ) ;
#7412=AXIS2_PLACEMENT_3D ( 'NONE', #6917, #22436, #18131 ) ;
#7530=AXIS2_PLACEMENT_3D ( 'NONE', #19040, #27789, #21765 ) ;
#7533=CARTESIAN_POINT ( 'NONE',  ( 162.7359358511135952, 208.5633933773887350, -140.4786076439499709 ) ) ;
#7549=EDGE_CURVE ( 'NONE', #19026, #11671, #16987, .T. ) ;
#7571=CIRCLE ( 'NONE', #10761, 562.1290781602207289 ) ;
#7578=DIRECTION ( 'NONE',  ( 0.8660254037844432595, 0.4999999999999919509, -0.000000000000000000 ) ) ;
#7629=DIRECTION ( 'NONE',  ( -0.000000000000000000, -0.000000000000000000, -1.000000000000000000 ) ) ;
#7633=CARTESIAN_POINT ( 'NONE',  ( 111.8061829044033004, 200.9721503227722508, -148.4939404368777218 ) ) ;
#7677=DIRECTION ( 'NONE',  ( -0.8660254037844363761, 0.5000000000000041078, -0.000000000000000000 ) ) ;
#7678=CARTESIAN_POINT ( 'NONE',  ( 134.9999999999998579, 467.1080826427131001, -145.0000000000000000 ) ) ;
#7679=CARTESIAN_POINT ( 'NONE',  ( 136.5616572741750474, 249.9618117005867077, -139.1934629298939115 ) ) ;
#7697=EDGE_CURVE ( 'NONE', #24318, #8004, #17482, .T. ) ;
#7708=DIRECTION ( 'NONE',  ( -0.8660254037844431485, -0.4999999999999922284, 0.000000000000000000 ) ) ;
#7711=ADVANCED_FACE ( 'NONE', ( #5188 ), #12380, .T. ) ;
#7735=CARTESIAN_POINT ( 'NONE',  ( 134.9999999999998579, 250.0000000000000568, -138.9999999999999432 ) ) ;
#7758=DIRECTION ( 'NONE',  ( -1.000000000000000000, 0.000000000000000000, 0.000000000000000000 ) ) ;
#7770=TOROIDAL_SURFACE ( 'NONE', #878, -538.1631314933625845, 562.1290781602207289 ) ;
#7793=ORIENTED_EDGE ( 'NONE', *, *, #20537, .F. ) ;
#7833=DIRECTION ( 'NONE',  ( -0.000000000000000000, -1.000000000000000000, -0.000000000000000000 ) ) ;
#7866=CARTESIAN_POINT ( 'NONE',  ( 134.9999999999998579, 455.5353319318992362, -127.0692718809191035 ) ) ;
#7872=CARTESIAN_POINT ( 'NONE',  ( 129.1910320842563067, 249.4323282239753325, -146.5522648598510216 ) ) ;
#7903=CIRCLE ( 'NONE', #18357, 6.000000000000005329 ) ;
#7906=CARTESIAN_POINT ( 'NONE',  ( 110.4484086432434822, 202.7590692334812559, -139.6159404653925549 ) ) ;
#7960=ORIENTED_EDGE ( 'NONE', *, *, #1378, .F. ) ;
#7989=DIRECTION ( 'NONE',  ( 0.4999999999999919509, -0.8660254037844432595, -0.000000000000000000 ) ) ;
#8004=VERTEX_POINT ( 'NONE', #3726 ) ;
#8014=CARTESIAN_POINT ( 'NONE',  ( 134.6025894306528699, 250.0000000000000568, -151.0000000000000284 ) ) ;
#8021=CARTESIAN_POINT ( 'NONE',  ( 106.6443156122982572, 210.2031273749746276, -143.0663072493379104 ) ) ;
#8040=AXIS2_PLACEMENT_3D ( 'NONE', #8587, #13052, #13466 ) ;
#8047=CARTESIAN_POINT ( 'NONE',  ( 112.0145559484521414, 200.7200133411070908, -141.9885977063034943 ) ) ;
#8059=AXIS2_PLACEMENT_3D ( 'NONE', #2194, #2336, #26053 ) ;
#8154=CARTESIAN_POINT ( 'NONE',  ( 129.7913655954319836, 249.5452024337660646, -148.0040471605077812 ) ) ;
#8157=PLANE ( 'NONE',  #6932 ) ;
#8177=CIRCLE ( 'NONE', #7270, 30.00000000000001421 ) ;
#8186=CARTESIAN_POINT ( 'NONE',  ( 110.6502358794795100, 202.4751799119059115, -139.8013169873308641 ) ) ;
#8221=FACE_OUTER_BOUND ( 'NONE', #17140, .T. ) ;
#8295=CARTESIAN_POINT ( 'NONE',  ( 134.9999999999998579, 467.1080826427131001, -145.0000000000000000 ) ) ;
#8305=FACE_OUTER_BOUND ( 'NONE', #14535, .T. ) ;
#8317=ORIENTED_EDGE ( 'NONE', *, *, #13514, .T. ) ;
#8328=EDGE_CURVE ( 'NONE', #18109, #5589, #11561, .T. ) ;
#8341=TOROIDAL_SURFACE ( 'NONE', #13859, -538.1631314933625845, 562.1290781602207289 ) ;
#8347=EDGE_LOOP ( 'NONE', ( #19447, #10257 ) ) ;
#8379=EDGE_LOOP ( 'NONE', ( #4589, #18360, #9602, #22482 ) ) ;
#8382=ADVANCED_FACE ( 'NONE', ( #14780 ), #8341, .T. ) ;
#8385=EDGE_CURVE ( 'NONE', #2973, #23432, #7007, .T. ) ;
#8396=ORIENTED_EDGE ( 'NONE', *, *, #9470, .T. ) ;
#8404=DIRECTION ( 'NONE',  ( 0.000000000000000000, 0.000000000000000000, 1.000000000000000000 ) ) ;
#8443=CARTESIAN_POINT ( 'NONE',  ( 134.9999999999998863, 250.0000000000000568, -151.0000000000000284 ) ) ;
#8470=EDGE_CURVE ( 'NONE', #20045, #5588, #28049, .T. ) ;
#8507=CARTESIAN_POINT ( 'NONE',  ( 160.8827288317913826, 204.8302013751908532, -138.9999999999999716 ) ) ;
#8527=AXIS2_PLACEMENT_3D ( 'NONE', #16131, #3034, #24881 ) ;
#8558=DIRECTION ( 'NONE',  ( 1.000000000000000000, 0.000000000000000000, 0.000000000000000000 ) ) ;
#8587=CARTESIAN_POINT ( 'NONE',  ( 134.9999999999998579, 220.0000000000000284, -169.9999999999999716 ) ) ;
#8593=CARTESIAN_POINT ( 'NONE',  ( 156.5461074670752453, 207.5603490538953224, -145.0000000000000000 ) ) ;
#8601=AXIS2_PLACEMENT_3D ( 'NONE', #23867, #17, #8777 ) ;
#8632=ORIENTED_EDGE ( 'NONE', *, *, #20283, .T. ) ;
#8646=DIRECTION ( 'NONE',  ( 6.123233995736667428E-17, -1.060575238724912585E-16, -1.000000000000000000 ) ) ;
#8654=VECTOR ( 'NONE', #637, 1000.000000000000000 ) ;
#8658=ORIENTED_EDGE ( 'NONE', *, *, #24700, .F. ) ;
#8664=ADVANCED_FACE ( 'NONE', ( #3527 ), #13883, .T. ) ;
#8692=ORIENTED_EDGE ( 'NONE', *, *, #8385, .F. ) ;
#8709=ADVANCED_FACE ( 'NONE', ( #25931 ), #2841, .T. ) ;
#8736=ORIENTED_EDGE ( 'NONE', *, *, #3737, .T. ) ;
#8759=CARTESIAN_POINT ( 'NONE',  ( 109.4209008705013417, 204.3200822355380240, -150.9609010065648818 ) ) ;
#8777=DIRECTION ( 'NONE',  ( 0.000000000000000000, 1.000000000000000000, 0.000000000000000000 ) ) ;
#8784=CARTESIAN_POINT ( 'NONE',  ( 159.5478513586114389, 202.7507791982433787, -150.3903514073974179 ) ) ;
#8819=CARTESIAN_POINT ( 'NONE',  ( 134.9999999999998579, 220.0000000000000284, -122.9999999999999574 ) ) ;
#8827=LINE ( 'NONE', #5964, #5446 ) ;
#8854=MANIFOLD_SOLID_BREP ( 'Chamfer2', #22359 ) ;
#8878=DIRECTION ( 'NONE',  ( 0.000000000000000000, 0.000000000000000000, -1.000000000000000000 ) ) ;
#8930=CARTESIAN_POINT ( 'NONE',  ( 157.9898533828750260, 200.7262996950787510, -141.9943226514403420 ) ) ;
#8944=AXIS2_PLACEMENT_3D ( 'NONE', #24511, #1955, #13318 ) ;
#8973=ORIENTED_EDGE ( 'NONE', *, *, #4077, .F. ) ;
#8995=CIRCLE ( 'NONE', #14061, 6.000000000000005329 ) ;
#9000=DIRECTION ( 'NONE',  ( 0.000000000000000000, 0.000000000000000000, 1.000000000000000000 ) ) ;
#9004=DIRECTION ( 'NONE',  ( 0.000000000000000000, 0.000000000000000000, -1.000000000000000000 ) ) ;
#9006=LINE ( 'NONE', #21798, #17224 ) ;
#9015=DIRECTION ( 'NONE',  ( 1.000000000000000000, 0.000000000000000000, 0.000000000000000000 ) ) ;
#9019=VECTOR ( 'NONE', #26060, 1000.000000000000000 ) ;
#9025=EDGE_CURVE ( 'NONE', #13229, #15076, #4699, .T. ) ;
#9033=CARTESIAN_POINT ( 'NONE',  ( 134.9999999999998579, 404.6636166603179277, -145.0000000000000000 ) ) ;
#9046=DIRECTION ( 'NONE',  ( -0.000000000000000000, -1.000000000000000000, -0.000000000000000000 ) ) ;
#9048=CARTESIAN_POINT ( 'NONE',  ( -68.97958094182604327, 102.2323340340523288, -127.0692718809191035 ) ) ;
#9072=CARTESIAN_POINT ( 'NONE',  ( 160.4757310268322499, 204.1562516397053173, -139.0778438077165902 ) ) ;
#9120=CARTESIAN_POINT ( 'NONE',  ( 140.7972055090965853, 249.4346022597576393, -146.5591841905931290 ) ) ;
#9121=ORIENTED_EDGE ( 'NONE', *, *, #2322, .F. ) ;
#9142=DIRECTION ( 'NONE',  ( 0.000000000000000000, 0.000000000000000000, -1.000000000000000000 ) ) ;
#9164=DIRECTION ( 'NONE',  ( -0.8660254037844362651, 0.5000000000000039968, -0.000000000000000000 ) ) ;
#9249=CARTESIAN_POINT ( 'NONE',  ( 109.0192378864665557, 205.0000000000002558, -138.9999999999999432 ) ) ;
#9266=CARTESIAN_POINT ( 'NONE',  ( 134.9999999999998579, 467.1080826427131001, -134.2811822434184705 ) ) ;
#9268=CARTESIAN_POINT ( 'NONE',  ( 139.7676321182949835, 249.6195736766799484, -148.6640466283485296 ) ) ;
#9304=CARTESIAN_POINT ( 'NONE',  ( 106.8135592195724826, 209.7270530936113175, -141.9943226514401999 ) ) ;
#9320=DIRECTION ( 'NONE',  ( -0.4383711467890776259, 0.000000000000000000, 0.8987940462991669266 ) ) ;
#9332=AXIS2_PLACEMENT_3D ( 'NONE', #21935, #26242, #19502 ) ;
#9387=AXIS2_PLACEMENT_3D ( 'NONE', #316, #13681, #13249 ) ;
#9414=FACE_OUTER_BOUND ( 'NONE', #10038, .T. ) ;
#9416=CARTESIAN_POINT ( 'NONE',  ( 141.0001535789425020, 249.3938455642302756, -144.6099047286054713 ) ) ;
#9446=CARTESIAN_POINT ( 'NONE',  ( -79.00187704905530950, 96.44595867864546790, -145.0000000000000000 ) ) ;
#9470=EDGE_CURVE ( 'NONE', #21067, #23466, #23540, .T. ) ;
#9508=DIRECTION ( 'NONE',  ( -1.000000000000000000, 0.000000000000000000, -0.000000000000000000 ) ) ;
#9534=EDGE_LOOP ( 'NONE', ( #18774, #19196 ) ) ;
#9539=DIRECTION ( 'NONE',  ( 0.4999999999999919509, -0.8660254037844432595, -0.000000000000000000 ) ) ;
#9544=CIRCLE ( 'NONE', #15058, 562.1290781602207289 ) ;
#9557=CARTESIAN_POINT ( 'NONE',  ( 136.5548239485688953, 249.9602781967704743, -150.7983993365949971 ) ) ;
#9564=EDGE_LOOP ( 'NONE', ( #27333, #1746 ) ) ;
#9567=DIRECTION ( 'NONE',  ( -0.8660254037844362651, 0.5000000000000039968, 0.000000000000000000 ) ) ;
#9575=DIRECTION ( 'NONE',  ( 0.000000000000000000, 0.000000000000000000, -1.000000000000000000 ) ) ;
#9602=ORIENTED_EDGE ( 'NONE', *, *, #23793, .T. ) ;
#9633=ORIENTED_EDGE ( 'NONE', *, *, #26461, .T. ) ;
#9636=DIRECTION ( 'NONE',  ( 0.000000000000000000, -0.000000000000000000, -1.000000000000000000 ) ) ;
#9640=CARTESIAN_POINT ( 'NONE',  ( 134.9999999999998579, 220.0000000000000284, -169.9999999999999716 ) ) ;
#9646=FACE_BOUND ( 'NONE', #10821, .T. ) ;
#9666=DIRECTION ( 'NONE',  ( -0.8660254037844362651, 0.5000000000000039968, -0.000000000000000000 ) ) ;
#9682=CARTESIAN_POINT ( 'NONE',  ( 162.3518214533014543, 207.6748957395177229, -139.8013169873308073 ) ) ;
#9696=( NAMED_UNIT ( * ) PLANE_ANGLE_UNIT ( ) SI_UNIT ( $, .RADIAN. ) );
#9698=ADVANCED_FACE ( 'NONE', ( #19188 ), #25793, .T. ) ;
#9711=EDGE_CURVE ( 'NONE', #3815, #4843, #1664, .T. ) ;
#9729=DIRECTION ( 'NONE',  ( 0.8660254037844432595, 0.4999999999999918954, 0.000000000000000000 ) ) ;
#9764=CARTESIAN_POINT ( 'NONE',  ( 134.9999999999998863, 537.6859242279716682, -145.0000000000000000 ) ) ;
#9791=CARTESIAN_POINT ( 'NONE',  ( 109.2152537968686232, 204.6604904840920653, -138.9999999999999432 ) ) ;
#9823=CARTESIAN_POINT ( 'NONE',  ( 163.0358885901997326, 209.3211669751875377, -141.3391815462163379 ) ) ;
#9874=CIRCLE ( 'NONE', #23176, 7.999999999999979572 ) ;
#9875=AXIS2_PLACEMENT_3D ( 'NONE', #603, #2887, #9508 ) ;
#9900=AXIS2_PLACEMENT_3D ( 'NONE', #13614, #26658, #680 ) ;
#9904=DIRECTION ( 'NONE',  ( -0.000000000000000000, -0.000000000000000000, 1.000000000000000000 ) ) ;
#9931=VERTEX_POINT ( 'NONE', #2796 ) ;
#9935=ORIENTED_EDGE ( 'NONE', *, *, #10766, .F. ) ;
#9958=CARTESIAN_POINT ( 'NONE',  ( 161.9784637521712227, 206.8776822256648984, -150.6145052419836077 ) ) ;
#9960=EDGE_CURVE ( 'NONE', #5589, #18109, #24390, .T. ) ;
#9980=DIRECTION ( 'NONE',  ( 0.000000000000000000, 0.000000000000000000, 1.000000000000000000 ) ) ;
#9996=CARTESIAN_POINT ( 'NONE',  ( 134.9999999999998579, 220.0000000000000284, -119.9999999999999858 ) ) ;
#10038=EDGE_LOOP ( 'NONE', ( #17107, #8396, #7157, #17582 ) ) ;
#10043=ORIENTED_EDGE ( 'NONE', *, *, #11291, .F. ) ;
#10057=VECTOR ( 'NONE', #452, 1000.000000000000000 ) ;
#10102=CARTESIAN_POINT ( 'NONE',  ( 162.6214317851641908, 208.2882202355792742, -149.7646631383025237 ) ) ;
#10104=AXIS2_PLACEMENT_3D ( 'NONE', #3373, #7833, #27913 ) ;
#10118=CARTESIAN_POINT ( 'NONE',  ( 135.7863972241894430, 249.9903379835593853, -139.0484678162419812 ) ) ;
#10148=AXIS2_PLACEMENT_3D ( 'NONE', #23309, #5921, #25735 ) ;
#10190=( GEOMETRIC_REPRESENTATION_CONTEXT ( 3 ) GLOBAL_UNCERTAINTY_ASSIGNED_CONTEXT ( ( #4295 ) ) GLOBAL_UNIT_ASSIGNED_CONTEXT ( ( #4198, #19579, #15424 ) ) REPRESENTATION_CONTEXT ( 'NONE', 'WORKASPACE' ) );
#10257=ORIENTED_EDGE ( 'NONE', *, *, #22618, .T. ) ;
#10265=ORIENTED_EDGE ( 'NONE', *, *, #11291, .T. ) ;
#10268=ORIENTED_EDGE ( 'NONE', *, *, #3737, .F. ) ;
#10274=FACE_OUTER_BOUND ( 'NONE', #15409, .T. ) ;
#10313=CARTESIAN_POINT ( 'NONE',  ( 129.1547762805313937, 249.4250724608095595, -143.6319245046325079 ) ) ;
#10321=DIRECTION ( 'NONE',  ( 0.000000000000000000, 0.000000000000000000, -1.000000000000000000 ) ) ;
#10380=CARTESIAN_POINT ( 'NONE',  ( 162.3566490199804946, 207.6824095899247880, -150.2048413890044003 ) ) ;
#10387=ORIENTED_EDGE ( 'NONE', *, *, #18850, .T. ) ;
#10394=CARTESIAN_POINT ( 'NONE',  ( 350.4502000556478265, 95.60976900091161212, -145.0000000000000000 ) ) ;
#10423=FACE_OUTER_BOUND ( 'NONE', #16109, .T. ) ;
#10454=DIRECTION ( 'NONE',  ( -0.000000000000000000, 0.000000000000000000, -1.000000000000000000 ) ) ;
#10456=FACE_OUTER_BOUND ( 'NONE', #8379, .T. ) ;
#10506=ORIENTED_EDGE ( 'NONE', *, *, #15132, .F. ) ;
#10521=DIRECTION ( 'NONE',  ( 0.000000000000000000, 0.000000000000000000, -1.000000000000000000 ) ) ;
#10595=CARTESIAN_POINT ( 'NONE',  ( 130.4856197046055684, 249.6586625914459034, -148.9571385985324525 ) ) ;
#10599=CARTESIAN_POINT ( 'NONE',  ( 134.9999999999998579, 220.0000000000000284, -169.9999999999999716 ) ) ;
#10601=ADVANCED_FACE ( 'NONE', ( #13812, #864 ), #16248, .T. ) ;
#10637=AXIS2_PLACEMENT_3D ( 'NONE', #25065, #2320, #14860 ) ;
#10653=CARTESIAN_POINT ( 'NONE',  ( 104.9999999999998579, 220.0000000000000284, -169.9999999999999716 ) ) ;
#10662=CARTESIAN_POINT ( 'NONE',  ( 158.2656979116527793, 201.0591520573188973, -141.3400049877799063 ) ) ;
#10673=AXIS2_PLACEMENT_3D ( 'NONE', #15816, #24560, #1131 ) ;
#10697=DIRECTION ( 'NONE',  ( 0.7071067811865489050, 8.659560562354948882E-17, -0.7071067811865462405 ) ) ;
#10707=CIRCLE ( 'NONE', #144, 10.71881775658151170 ) ;
#10717=DIRECTION ( 'NONE',  ( -0.8660254037844363761, 0.5000000000000041078, -0.000000000000000000 ) ) ;
#10738=FACE_OUTER_BOUND ( 'NONE', #5315, .T. ) ;
#10748=CARTESIAN_POINT ( 'NONE',  ( 319.9779125536060178, 113.2029523930392969, -145.0000000000000000 ) ) ;
#10752=CARTESIAN_POINT ( 'NONE',  ( 107.3817056362660907, 208.2809019521421305, -149.7704424372629717 ) ) ;
#10761=AXIS2_PLACEMENT_3D ( 'NONE', #21057, #7989, #9729 ) ;
#10766=EDGE_CURVE ( 'NONE', #1235, #1528, #1488, .T. ) ;
#10821=EDGE_LOOP ( 'NONE', ( #26299, #3110 ) ) ;
#10877=CIRCLE ( 'NONE', #23728, 10.71881775658151170 ) ;
#10884=DIRECTION ( 'NONE',  ( -1.000000000000000000, 0.000000000000000000, 0.000000000000000000 ) ) ;
#10886=DIRECTION ( 'NONE',  ( 0.5000000000000039968, 0.8660254037844364872, 0.000000000000000000 ) ) ;
#10948=DIRECTION ( 'NONE',  ( -0.8660254037844432595, -0.4999999999999920064, 0.000000000000000000 ) ) ;
#11002=ORIENTED_EDGE ( 'NONE', *, *, #20379, .T. ) ;
#11033=CARTESIAN_POINT ( 'NONE',  ( 107.8677974404447752, 207.1985680636095424, -139.5328759577091660 ) ) ;
#11082=DIRECTION ( 'NONE',  ( -1.000000000000000000, 0.000000000000000000, 0.000000000000000000 ) ) ;
#11086=CARTESIAN_POINT ( 'NONE',  ( 157.8121286602244027, 200.5163485565246049, -142.5205423047663373 ) ) ;
#11088=AXIS2_PLACEMENT_3D ( 'NONE', #14924, #27826, #6005 ) ;
#11094=ORIENTED_EDGE ( 'NONE', *, *, #23822, .T. ) ;
#11106=AXIS2_PLACEMENT_3D ( 'NONE', #14028, #9980, #25343 ) ;
#11125=LINE ( 'NONE', #15166, #9019 ) ;
#11134=ORIENTED_EDGE ( 'NONE', *, *, #9025, .T. ) ;
#11135=CARTESIAN_POINT ( 'NONE',  ( 134.9999999999998579, 244.8793018922092699, -138.9999999999999432 ) ) ;
#11137=CARTESIAN_POINT ( 'NONE',  ( 140.6827089022704911, 249.4569214521288245, -146.9353207969096786 ) ) ;
#11157=CARTESIAN_POINT ( 'NONE',  ( 349.0018770490533484, 96.44595867864246941, -145.0000000000000000 ) ) ;
#11171=DIRECTION ( 'NONE',  ( -0.8660254037844363761, 0.5000000000000041078, -0.000000000000000000 ) ) ;
#11234=CARTESIAN_POINT ( 'NONE',  ( 159.9606642740977520, 203.3537529630600034, -139.3072807822095456 ) ) ;
#11262=ORIENTED_EDGE ( 'NONE', *, *, #1303, .F. ) ;
#11276=VERTEX_POINT ( 'NONE', #18521 ) ;
#11287=CARTESIAN_POINT ( 'NONE',  ( 139.7704065317532809, 249.6191093996066286, -141.3400049877799631 ) ) ;
#11291=EDGE_CURVE ( 'NONE', #17958, #1877, #1407, .T. ) ;
#11293=EDGE_LOOP ( 'NONE', ( #7960, #22860, #1170, #11328, #3289 ) ) ;
#11315=CARTESIAN_POINT ( 'NONE',  ( 134.9999999999998579, 220.0000000000000284, -189.9999999999999716 ) ) ;
#11323=CARTESIAN_POINT ( 'NONE',  ( 106.7205985613565105, 209.9859427875843778, -142.5205423047663942 ) ) ;
#11328=ORIENTED_EDGE ( 'NONE', *, *, #21711, .T. ) ;
#11335=VERTEX_POINT ( 'NONE', #18793 ) ;
#11356=ORIENTED_EDGE ( 'NONE', *, *, #2998, .F. ) ;
#11411=CONICAL_SURFACE ( 'NONE', #27434, 30.00000000000001421, 0.4537856055185259252 ) ;
#11412=ADVANCED_FACE ( 'NONE', ( #8305 ), #25963, .T. ) ;
#11419=CARTESIAN_POINT ( 'NONE',  ( 161.7276425571222092, 206.3697252471818615, -139.1927212198768871 ) ) ;
#11443=EDGE_CURVE ( 'NONE', #19844, #27008, #15303, .T. ) ;
#11458=CIRCLE ( 'NONE', #21525, 7.999999999999979572 ) ;
#11462=CARTESIAN_POINT ( 'NONE',  ( -24.92338318254761020, 127.6681916698425567, -145.0000000000000000 ) ) ;
#11471=CARTESIAN_POINT ( 'NONE',  ( 108.5410459154004172, 205.8592439309313136, -139.0778438077165902 ) ) ;
#11515=ADVANCED_FACE ( 'NONE', ( #12630, #10456 ), #19217, .T. ) ;
#11518=LINE ( 'NONE', #7337, #16362 ) ;
#11561=CIRCLE ( 'NONE', #11088, 10.00000000000000888 ) ;
#11579=CARTESIAN_POINT ( 'NONE',  ( 140.9608704376672108, 249.4019415319914117, -144.2111520032348722 ) ) ;
#11608=DIRECTION ( 'NONE',  ( 0.000000000000000000, 0.000000000000000000, -1.000000000000000000 ) ) ;
#11614=DIRECTION ( 'NONE',  ( 0.000000000000000000, 0.000000000000000000, -1.000000000000000000 ) ) ;
#11671=VERTEX_POINT ( 'NONE', #4829 ) ;
#11759=AXIS2_PLACEMENT_3D ( 'NONE', #26613, #25043, #11980 ) ;
#11761=ORIENTED_EDGE ( 'NONE', *, *, #7697, .F. ) ;
#11787=FACE_OUTER_BOUND ( 'NONE', #11293, .T. ) ;
#11809=CARTESIAN_POINT ( 'NONE',  ( 134.9999999999998579, 404.6636166603179277, -138.9999999999999716 ) ) ;
#11814=EDGE_CURVE ( 'NONE', #1235, #20045, #20361, .T. ) ;
#11820=CARTESIAN_POINT ( 'NONE',  ( 294.9233831825460470, 127.6681916698403398, -145.0000000000000000 ) ) ;
#11920=DIRECTION ( 'NONE',  ( 0.8660254037844432595, 0.4999999999999919509, -0.000000000000000000 ) ) ;
#11939=ADVANCED_FACE ( 'NONE', ( #10423 ), #24030, .T. ) ;
#11951=CARTESIAN_POINT ( 'NONE',  ( 111.4893267626885205, 201.3648822632117117, -149.1019530262190358 ) ) ;
#11956=FACE_OUTER_BOUND ( 'NONE', #14353, .T. ) ;
#11969=ORIENTED_EDGE ( 'NONE', *, *, #13521, .T. ) ;
#11980=DIRECTION ( 'NONE',  ( 0.000000000000000000, 0.000000000000000000, -1.000000000000000000 ) ) ;
#11987=CARTESIAN_POINT ( 'NONE',  ( 349.0018770490533484, 96.44595867864246941, -145.0000000000000000 ) ) ;
#11998=CARTESIAN_POINT ( 'NONE',  ( 134.9999999999998579, 250.0000000000000568, -138.9999999999999432 ) ) ;
#12002=AXIS2_PLACEMENT_3D ( 'NONE', #11315, #22511, #10884 ) ;
#12048=AXIS2_PLACEMENT_3D ( 'NONE', #5023, #22563, #9636 ) ;
#12055=CARTESIAN_POINT ( 'NONE',  ( 134.9999999999998863, 537.6859242279716682, -145.0000000000000000 ) ) ;
#12061=DIRECTION ( 'NONE',  ( 0.000000000000000000, 0.000000000000000000, -1.000000000000000000 ) ) ;
#12096=CARTESIAN_POINT ( 'NONE',  ( 111.2276402061722109, 201.6982782665056675, -140.4786076439499425 ) ) ;
#12156=ORIENTED_EDGE ( 'NONE', *, *, #25981, .F. ) ;
#12162=CARTESIAN_POINT ( 'NONE',  ( -80.45020005564978760, 95.60976900091465325, -145.0000000000000000 ) ) ;
#12170=DIRECTION ( 'NONE',  ( 1.000000000000000000, 0.000000000000000000, -1.224646799147353207E-16 ) ) ;
#12185=CIRCLE ( 'NONE', #8944, 10.53396790234563518 ) ;
#12192=AXIS2_PLACEMENT_3D ( 'NONE', #6499, #25607, #1623 ) ;
#12204=DIRECTION ( 'NONE',  ( -0.000000000000000000, -1.000000000000000000, -0.000000000000000000 ) ) ;
#12270=CARTESIAN_POINT ( 'NONE',  ( 163.0755097476689741, 209.4274900230976471, -148.4939404368777787 ) ) ;
#12286=CIRCLE ( 'NONE', #19606, 6.000000000000005329 ) ;
#12300=AXIS2_PLACEMENT_3D ( 'NONE', #23592, #10521, #19279 ) ;
#12332=CARTESIAN_POINT ( 'NONE',  ( 134.9999999999998579, 468.7804619981748147, -145.0000000000000000 ) ) ;
#12361=ORIENTED_EDGE ( 'NONE', *, *, #8470, .T. ) ;
#12380=CYLINDRICAL_SURFACE ( 'NONE', #2803, 6.000000000000032863 ) ;
#12398=AXIS2_PLACEMENT_3D ( 'NONE', #6574, #26102, #9015 ) ;
#12410=CARTESIAN_POINT ( 'NONE',  ( 161.8971595647778088, 206.7117171029577207, -150.6809294437986466 ) ) ;
#12412=AXIS2_PLACEMENT_3D ( 'NONE', #525, #13900, #9575 ) ;
#12413=DIRECTION ( 'NONE',  ( -1.000000000000000000, 0.000000000000000000, 0.000000000000000000 ) ) ;
#12462=DIRECTION ( 'NONE',  ( 0.4999999999999920064, -0.8660254037844432595, 0.000000000000000000 ) ) ;
#12483=CARTESIAN_POINT ( 'NONE',  ( 132.3338888694437401, 249.8834866143649833, -150.3892986974657617 ) ) ;
#12515=CARTESIAN_POINT ( 'NONE',  ( 111.7303663796180473, 201.0648462552355795, -148.6534330424975963 ) ) ;
#12572=ORIENTED_EDGE ( 'NONE', *, *, #1722, .F. ) ;
#12614=AXIS2_PLACEMENT_3D ( 'NONE', #13861, #9539, #22610 ) ;
#12623=DIRECTION ( 'NONE',  ( 0.000000000000000000, 0.000000000000000000, -1.000000000000000000 ) ) ;
#12626=CARTESIAN_POINT ( 'NONE',  ( 129.3841014818332553, 249.4697745299731935, -142.8785553633037466 ) ) ;
#12630=FACE_BOUND ( 'NONE', #178, .T. ) ;
#12634=DIRECTION ( 'NONE',  ( 0.8660254037844432595, 0.4999999999999919509, -0.000000000000000000 ) ) ;
#12733=CIRCLE ( 'NONE', #8601, 35.18636678425507114 ) ;
#12742=ORIENTED_EDGE ( 'NONE', *, *, #5358, .T. ) ;
#12747=ORIENTED_EDGE ( 'NONE', *, *, #1414, .T. ) ;
#12762=CARTESIAN_POINT ( 'NONE',  ( 131.0364239427135544, 249.7383283561057112, -140.4786076439499709 ) ) ;
#12771=FACE_BOUND ( 'NONE', #9564, .T. ) ;
#12833=DIRECTION ( 'NONE',  ( 0.4383711467890776259, -5.368498217537984310E-17, 0.8987940462991669266 ) ) ;
#12844=DIRECTION ( 'NONE',  ( -0.8660254037844362651, 0.5000000000000039968, -0.000000000000000000 ) ) ;
#12853=DIRECTION ( 'NONE',  ( 0.000000000000000000, 0.000000000000000000, 1.000000000000000000 ) ) ;
#12871=CARTESIAN_POINT ( 'NONE',  ( 124.2811822434183284, 467.1080826427131001, -145.0000000000000000 ) ) ;
#12881=ADVANCED_FACE ( 'NONE', ( #21805, #12771, #2114 ), #19647, .T. ) ;
#12904=CARTESIAN_POINT ( 'NONE',  ( 131.9890216985461961, 249.8503482187554425, -150.2048413890044287 ) ) ;
#12914=CARTESIAN_POINT ( 'NONE',  ( 108.2762260028630976, 206.3663779394882170, -150.7983993365949686 ) ) ;
#12931=CARTESIAN_POINT ( 'NONE',  ( 144.9999999999998863, 220.0000000000000284, -119.9999999999999858 ) ) ;
#12944=PRODUCT_DEFINITION_FORMATION_WITH_SPECIFIED_SOURCE ( 'ANY', '', #21502, .NOT_KNOWN. ) ;
#13030=DIRECTION ( 'NONE',  ( 0.000000000000000000, -0.000000000000000000, -1.000000000000000000 ) ) ;
#13052=DIRECTION ( 'NONE',  ( -0.000000000000000000, -0.000000000000000000, 1.000000000000000000 ) ) ;
#13057=EDGE_LOOP ( 'NONE', ( #9121, #5702, #26427, #14331, #24298 ) ) ;
#13061=CARTESIAN_POINT ( 'NONE',  ( 109.0192378864665557, 205.0000000000002558, -138.9999999999999432 ) ) ;
#13069=AXIS2_PLACEMENT_3D ( 'NONE', #457, #28302, #15689 ) ;
#13080=EDGE_CURVE ( 'NONE', #5588, #21528, #7571, .T. ) ;
#13092=ORIENTED_EDGE ( 'NONE', *, *, #3117, .F. ) ;
#13111=ORIENTED_EDGE ( 'NONE', *, *, #18015, .T. ) ;
#13117=CARTESIAN_POINT ( 'NONE',  ( 157.9841506265077555, 200.7184471377001103, -148.0084258618598199 ) ) ;
#13177=EDGE_LOOP ( 'NONE', ( #28190, #16968, #14734, #2425 ) ) ;
#13196=DIRECTION ( 'NONE',  ( -0.000000000000000000, -0.000000000000000000, 1.000000000000000000 ) ) ;
#13197=CARTESIAN_POINT ( 'NONE',  ( 107.0542349192081275, 209.0860837716736000, -141.0358260266775972 ) ) ;
#13229=VERTEX_POINT ( 'NONE', #17175 ) ;
#13246=CARTESIAN_POINT ( 'NONE',  ( 134.9999999999998579, 220.0000000000000284, -119.9999999999999858 ) ) ;
#13249=DIRECTION ( 'NONE',  ( -1.000000000000000000, 0.000000000000000000, 0.000000000000000000 ) ) ;
#13250=CARTESIAN_POINT ( 'NONE',  ( 157.6690878436907610, 200.3501690022571609, -146.9353207969096502 ) ) ;
#13272=CARTESIAN_POINT ( 'NONE',  ( 134.9999999999998579, 220.0000000000000284, 109.9999999999999858 ) ) ;
#13300=CARTESIAN_POINT ( 'NONE',  ( 136.9323230404753815, 249.9383011342688974, -150.6837522856750411 ) ) ;
#13303=ORIENTED_EDGE ( 'NONE', *, *, #9960, .T. ) ;
#13318=DIRECTION ( 'NONE',  ( 0.8660254037844359321, -0.5000000000000045519, 0.000000000000000000 ) ) ;
#13347=DIRECTION ( 'NONE',  ( 0.000000000000000000, 0.000000000000000000, -1.000000000000000000 ) ) ;
#13349=EDGE_CURVE ( 'NONE', #28280, #26741, #5340, .T. ) ;
#13390=CARTESIAN_POINT ( 'NONE',  ( 157.5598940431783603, 200.2249467617852190, -146.3660979730027520 ) ) ;
#13416=ORIENTED_EDGE ( 'NONE', *, *, #20319, .F. ) ;
#13439=CARTESIAN_POINT ( 'NONE',  ( 140.3919500952845283, 249.5118635391362716, -147.6607294899351075 ) ) ;
#13453=CIRCLE ( 'NONE', #16209, 7.999999999999979572 ) ;
#13466=DIRECTION ( 'NONE',  ( -1.000000000000000000, 0.000000000000000000, 0.000000000000000000 ) ) ;
#13514=EDGE_CURVE ( 'NONE', #212, #18655, #17663, .T. ) ;
#13520=VERTEX_POINT ( 'NONE', #10394 ) ;
#13521=EDGE_CURVE ( 'NONE', #24416, #7370, #21331, .T. ) ;
#13545=PLANE ( 'NONE',  #23388 ) ;
#13552=CONICAL_SURFACE ( 'NONE', #27286, 30.00000000000001421, 0.7853981633974500554 ) ;
#13585=LINE ( 'NONE', #11135, #18515 ) ;
#13587=CARTESIAN_POINT ( 'NONE',  ( 138.9634206111875301, 249.7383700032220304, -140.4781857268138765 ) ) ;
#13596=AXIS2_PLACEMENT_3D ( 'NONE', #11157, #241, #9142 ) ;
#13612=CARTESIAN_POINT ( 'NONE',  ( -79.00187704905530950, 96.44595867864546790, -145.0000000000000000 ) ) ;
#13614=CARTESIAN_POINT ( 'NONE',  ( 134.9999999999998579, 467.1080826427131001, -145.0000000000000000 ) ) ;
#13639=CIRCLE ( 'NONE', #26908, 562.1290781602207289 ) ;
#13663=ORIENTED_EDGE ( 'NONE', *, *, #2013, .F. ) ;
#13681=DIRECTION ( 'NONE',  ( -0.000000000000000000, -0.000000000000000000, -1.000000000000000000 ) ) ;
#13693=DIRECTION ( 'NONE',  ( 0.000000000000000000, 0.000000000000000000, -1.000000000000000000 ) ) ;
#13729=EDGE_CURVE ( 'NONE', #27008, #19224, #17228, .T. ) ;
#13733=CARTESIAN_POINT ( 'NONE',  ( 140.6935016229380722, 249.4551793339562096, -143.0663072493378536 ) ) ;
#13742=EDGE_LOOP ( 'NONE', ( #11002, #5515 ) ) ;
#13771=VERTEX_POINT ( 'NONE', #7363 ) ;
#13794=CIRCLE ( 'NONE', #10104, 17.93072811908088937 ) ;
#13798=DIRECTION ( 'NONE',  ( 0.000000000000000000, 0.000000000000000000, -1.000000000000000000 ) ) ;
#13812=FACE_OUTER_BOUND ( 'NONE', #21784, .T. ) ;
#13850=CIRCLE ( 'NONE', #12002, 20.24534822868278994 ) ;
#13859=AXIS2_PLACEMENT_3D ( 'NONE', #4129, #12634, #10321 ) ;
#13861=CARTESIAN_POINT ( 'NONE',  ( -70.31278697424053803, 101.4626071723526195, -152.5098566583459672 ) ) ;
#13865=DIRECTION ( 'NONE',  ( 0.000000000000000000, 0.000000000000000000, -1.000000000000000000 ) ) ;
#13877=CARTESIAN_POINT ( 'NONE',  ( 137.1196823444857671, 249.9255760664107413, -150.6165463336313053 ) ) ;
#13883=TOROIDAL_SURFACE ( 'NONE', #6981, -538.1631314933625845, 562.1290781602207289 ) ;
#13886=EDGE_LOOP ( 'NONE', ( #9633, #27968, #8973, #18046 ) ) ;
#13900=DIRECTION ( 'NONE',  ( 0.8660254037844432595, 0.4999999999999919509, -0.000000000000000000 ) ) ;
#13906=DIRECTION ( 'NONE',  ( 0.8660254037844432595, 0.4999999999999919509, -0.000000000000000000 ) ) ;
#13909=DIRECTION ( 'NONE',  ( 0.8660254037844432595, 0.4999999999999919509, -0.000000000000000000 ) ) ;
#13914=DIRECTION ( 'NONE',  ( 0.000000000000000000, 0.000000000000000000, -1.000000000000000000 ) ) ;
#13993=CIRCLE ( 'NONE', #12614, 10.53396790234565117 ) ;
#14027=ORIENTED_EDGE ( 'NONE', *, *, #18015, .F. ) ;
#14028=CARTESIAN_POINT ( 'NONE',  ( 134.9999999999998579, 220.0000000000000284, -119.9999999999999858 ) ) ;
#14030=ORIENTED_EDGE ( 'NONE', *, *, #2322, .T. ) ;
#14061=AXIS2_PLACEMENT_3D ( 'NONE', #2136, #26272, #15376 ) ;
#14124=ADVANCED_FACE ( 'NONE', ( #2062 ), #6238, .T. ) ;
#14164=CIRCLE ( 'NONE', #15534, 10.71881775658151170 ) ;
#14187=ORIENTED_EDGE ( 'NONE', *, *, #13514, .F. ) ;
#14208=CIRCLE ( 'NONE', #18326, 10.71881775658151170 ) ;
#14222=DIRECTION ( 'NONE',  ( 0.000000000000000000, 0.000000000000000000, 1.000000000000000000 ) ) ;
#14244=FACE_OUTER_BOUND ( 'NONE', #19126, .T. ) ;
#14247=CARTESIAN_POINT ( 'NONE',  ( 111.0465853079006848, 201.9350282673592858, -149.7646631383025237 ) ) ;
#14280=CARTESIAN_POINT ( 'NONE',  ( 163.3898168894218657, 210.3035215302631968, -143.4419542882358201 ) ) ;
#14331=ORIENTED_EDGE ( 'NONE', *, *, #1284, .T. ) ;
#14350=FACE_OUTER_BOUND ( 'NONE', #23095, .T. ) ;
#14353=EDGE_LOOP ( 'NONE', ( #1611, #10387 ) ) ;
#14384=CARTESIAN_POINT ( 'NONE',  ( 109.0192378864665557, 205.0000000000002558, -138.9999999999999432 ) ) ;
#14398=ORIENTED_EDGE ( 'NONE', *, *, #22133, .F. ) ;
#14417=FACE_OUTER_BOUND ( 'NONE', #13057, .T. ) ;
#14418=CARTESIAN_POINT ( 'NONE',  ( 162.7383316901385513, 208.5692331145191076, -149.5158039499305289 ) ) ;
#14423=CARTESIAN_POINT ( 'NONE',  ( 126.9999999999998579, 404.6636166603179277, -145.0000000000000000 ) ) ;
#14454=EDGE_CURVE ( 'NONE', #16059, #23894, #8995, .T. ) ;
#14465=CARTESIAN_POINT ( 'NONE',  ( 410.1240808061609187, 61.15703788601284430, -145.0000000000000000 ) ) ;
#14510=ORIENTED_EDGE ( 'NONE', *, *, #10766, .T. ) ;
#14530=EDGE_CURVE ( 'NONE', #21528, #7328, #26897, .T. ) ;
#14535=EDGE_LOOP ( 'NONE', ( #26831, #17664, #16004, #11262 ) ) ;
#14558=CARTESIAN_POINT ( 'NONE',  ( 163.3295226458395462, 210.1286235168210510, -142.8785553633037182 ) ) ;
#14581=EDGE_CURVE ( 'NONE', #26741, #28280, #27552, .T. ) ;
#14610=ORIENTED_EDGE ( 'NONE', *, *, #6752, .F. ) ;
#14615=DIRECTION ( 'NONE',  ( 0.000000000000000000, 0.000000000000000000, -1.000000000000000000 ) ) ;
#14627=CARTESIAN_POINT ( 'NONE',  ( 133.4403429179407681, 249.9619548141471057, -139.1927212198768586 ) ) ;
#14635=CARTESIAN_POINT ( 'NONE',  ( 106.7460014144458569, 209.9136339888866303, -147.6607294899350507 ) ) ;
#14683=AXIS2_PLACEMENT_3D ( 'NONE', #16525, #870, #7758 ) ;
#14734=ORIENTED_EDGE ( 'NONE', *, *, #20379, .F. ) ;
#14737=DIRECTION ( 'NONE',  ( 0.000000000000000000, 0.000000000000000000, 1.000000000000000000 ) ) ;
#14780=FACE_OUTER_BOUND ( 'NONE', #2753, .T. ) ;
#14791=EDGE_CURVE ( 'NONE', #7370, #24416, #6711, .T. ) ;
#14810=CARTESIAN_POINT ( 'NONE',  ( 112.5440210185366681, 200.1070613527027433, -144.6008566625276330 ) ) ;
#14845=CARTESIAN_POINT ( 'NONE',  ( 163.4430707983499076, 210.4607210870969709, -144.2074248490018249 ) ) ;
#14860=DIRECTION ( 'NONE',  ( 1.000000000000000000, 0.000000000000000000, 0.000000000000000000 ) ) ;
#14891=DIRECTION ( 'NONE',  ( 0.000000000000000000, 0.000000000000000000, -1.000000000000000000 ) ) ;
#14908=CARTESIAN_POINT ( 'NONE',  ( -70.31278697424053803, 101.4626071723526195, -145.0000000000000000 ) ) ;
#14916=CARTESIAN_POINT ( 'NONE',  ( 131.3377705351922202, 249.7774415780391450, -140.2311020877163230 ) ) ;
#14919=CARTESIAN_POINT ( 'NONE',  ( 134.9999999999998579, 467.1080826427131001, -155.7188177565815010 ) ) ;
#14924=CARTESIAN_POINT ( 'NONE',  ( 134.9999999999998579, 220.0000000000000284, -119.9999999999999858 ) ) ;
#14989=DIRECTION ( 'NONE',  ( 0.000000000000000000, -1.000000000000000000, -0.000000000000000000 ) ) ;
#15019=FACE_OUTER_BOUND ( 'NONE', #3595, .T. ) ;
#15037=ADVANCED_FACE ( 'NONE', ( #15019 ), #27802, .T. ) ;
#15058=AXIS2_PLACEMENT_3D ( 'NONE', #6455, #19953, #6600 ) ;
#15076=VERTEX_POINT ( 'NONE', #352 ) ;
#15093=VERTEX_POINT ( 'NONE', #15308 ) ;
#15132=EDGE_CURVE ( 'NONE', #24416, #2973, #11125, .T. ) ;
#15160=DIRECTION ( 'NONE',  ( 0.000000000000000000, 0.000000000000000000, 1.000000000000000000 ) ) ;
#15166=CARTESIAN_POINT ( 'NONE',  ( 113.4538925329242574, 207.5603490538955782, -151.0000000000000284 ) ) ;
#15172=CARTESIAN_POINT ( 'NONE',  ( 134.9999999999998579, 220.0000000000000284, -119.9999999999999858 ) ) ;
#15182=EDGE_LOOP ( 'NONE', ( #4928, #11094, #3449, #13092 ) ) ;
#15211=CARTESIAN_POINT ( 'NONE',  ( 106.5943545129268273, 210.3500852710297124, -146.3660979730027520 ) ) ;
#15238=CARTESIAN_POINT ( 'NONE',  ( 134.9999999999998579, 404.6636166603179277, -145.0000000000000000 ) ) ;
#15267=CARTESIAN_POINT ( 'NONE',  ( 160.1689500485674955, 203.6733438637415645, -150.7983993365949971 ) ) ;
#15297=CARTESIAN_POINT ( 'NONE',  ( 156.5461074670752453, 207.5603490538953224, -138.9999999999999432 ) ) ;
#15303=CIRCLE ( 'NONE', #9332, 562.1290781602207289 ) ;
#15308=CARTESIAN_POINT ( 'NONE',  ( 124.9999999999998579, 220.0000000000000284, 109.9999999999999858 ) ) ;
#15354=CARTESIAN_POINT ( 'NONE',  ( 108.1035950512893891, 206.7065541617666895, -139.3072807822095740 ) ) ;
#15360=ORIENTED_EDGE ( 'NONE', *, *, #7549, .T. ) ;
#15362=EDGE_CURVE ( 'NONE', #11671, #13771, #8177, .T. ) ;
#15376=DIRECTION ( 'NONE',  ( 0.000000000000000000, 0.000000000000000000, -1.000000000000000000 ) ) ;
#15408=CARTESIAN_POINT ( 'NONE',  ( 157.8620484902690180, 200.5745024719774392, -147.6607294899350791 ) ) ;
#15409=EDGE_LOOP ( 'NONE', ( #8736, #14030, #1080, #19680, #26360 ) ) ;
#15424=( NAMED_UNIT ( * ) SI_UNIT ( $, .STERADIAN. ) SOLID_ANGLE_UNIT ( ) );
#15443=AXIS2_PLACEMENT_3D ( 'NONE', #23349, #23633, #17162 ) ;
#15534=AXIS2_PLACEMENT_3D ( 'NONE', #9446, #13909, #4969 ) ;
#15546=CARTESIAN_POINT ( 'NONE',  ( 159.3469981926682806, 202.4713331616098912, -139.8040206391607398 ) ) ;
#15576=FACE_OUTER_BOUND ( 'NONE', #26939, .T. ) ;
#15598=CARTESIAN_POINT ( 'NONE',  ( 140.3821234321421230, 249.5134143970365983, -142.3407963099403162 ) ) ;
#15621=EDGE_CURVE ( 'NONE', #20045, #7328, #22396, .T. ) ;
#15629=ORIENTED_EDGE ( 'NONE', *, *, #26461, .F. ) ;
#15649=DIRECTION ( 'NONE',  ( -0.000000000000000000, -1.000000000000000000, -0.000000000000000000 ) ) ;
#15650=TOROIDAL_SURFACE ( 'NONE', #10148, 7.509856658345970715, 10.53396790234564762 ) ;
#15689=DIRECTION ( 'NONE',  ( 1.000000000000000000, 0.000000000000000000, 0.000000000000000000 ) ) ;
#15691=CARTESIAN_POINT ( 'NONE',  ( 158.4255425807448603, 201.2564237786189949, -148.9655004847909936 ) ) ;
#15723=CARTESIAN_POINT ( 'NONE',  ( 104.9999999999998579, 220.0000000000000284, -122.9999999999999574 ) ) ;
#15730=CARTESIAN_POINT ( 'NONE',  ( 109.0192378864665557, 205.0000000000002842, -151.0000000000000284 ) ) ;
#15757=ORIENTED_EDGE ( 'NONE', *, *, #25671, .F. ) ;
#15766=DIRECTION ( 'NONE',  ( -1.000000000000000000, 0.000000000000000000, 0.000000000000000000 ) ) ;
#15816=CARTESIAN_POINT ( 'NONE',  ( -68.97958094182604327, 102.2323340340523288, -145.0000000000000000 ) ) ;
#15825=ORIENTED_EDGE ( 'NONE', *, *, #23518, .F. ) ;
#15857=EDGE_CURVE ( 'NONE', #23432, #2973, #4726, .T. ) ;
#15936=AXIS2_PLACEMENT_3D ( 'NONE', #13272, #12853, #4350 ) ;
#15970=DIRECTION ( 'NONE',  ( -1.000000000000000000, 0.000000000000000000, 0.000000000000000000 ) ) ;
#16004=ORIENTED_EDGE ( 'NONE', *, *, #9025, .F. ) ;
#16031=EDGE_LOOP ( 'NONE', ( #25976, #2058, #9935, #11356 ) ) ;
#16059=VERTEX_POINT ( 'NONE', #23354 ) ;
#16088=DIRECTION ( 'NONE',  ( 1.000000000000000000, 0.000000000000000000, -1.224646799147353207E-16 ) ) ;
#16093=DIRECTION ( 'NONE',  ( 0.000000000000000000, 0.000000000000000000, -1.000000000000000000 ) ) ;
#16109=EDGE_LOOP ( 'NONE', ( #519, #2257, #2355, #22878, #23318 ) ) ;
#16131=CARTESIAN_POINT ( 'NONE',  ( 134.9999999999998579, 404.6636166603179277, -145.0000000000000000 ) ) ;
#16148=AXIS2_PLACEMENT_3D ( 'NONE', #4411, #7578, #13914 ) ;
#16185=TOROIDAL_SURFACE ( 'NONE', #3770, -538.1631314933625845, 562.1290781602207289 ) ;
#16191=AXIS2_PLACEMENT_3D ( 'NONE', #13612, #246, #9004 ) ;
#16209=AXIS2_PLACEMENT_3D ( 'NONE', #23116, #19324, #14891 ) ;
#16221=DIRECTION ( 'NONE',  ( 0.5000000000000039968, 0.8660254037844362651, 0.000000000000000000 ) ) ;
#16248=PLANE ( 'NONE',  #12048 ) ;
#16295=CARTESIAN_POINT ( 'NONE',  ( 162.9441897050832893, 209.0821077902480170, -141.0313312019551972 ) ) ;
#16338=CARTESIAN_POINT ( 'NONE',  ( -70.31278697424053803, 101.4626071723526195, -137.4901433416540328 ) ) ;
#16362=VECTOR ( 'NONE', #5024, 1000.000000000000000 ) ;
#16370=CARTESIAN_POINT ( 'NONE',  ( 134.9999999999998579, 244.8793018922092699, -145.0000000000000000 ) ) ;
#16400=CARTESIAN_POINT ( 'NONE',  ( 111.0430938661146030, 201.9396954599693572, -140.2311020877163514 ) ) ;
#16491=EDGE_LOOP ( 'NONE', ( #19777, #4474 ) ) ;
#16505=CARTESIAN_POINT ( 'NONE',  ( 134.2176099750896583, 249.9923178888783752, -139.0380470571626574 ) ) ;
#16509=CARTESIAN_POINT ( 'NONE',  ( 104.9999999999998579, 220.0000000000000284, -122.9999999999999574 ) ) ;
#16520=AXIS2_PLACEMENT_3D ( 'NONE', #21759, #21893, #2065 ) ;
#16525=CARTESIAN_POINT ( 'NONE',  ( 134.9999999999998579, 220.0000000000000284, -189.9999999999999716 ) ) ;
#16538=CARTESIAN_POINT ( 'NONE',  ( 112.2863758723266727, 200.4016019532060113, -142.8785553633036898 ) ) ;
#16616=( GEOMETRIC_REPRESENTATION_CONTEXT ( 3 ) GLOBAL_UNCERTAINTY_ASSIGNED_CONTEXT ( ( #5144 ) ) GLOBAL_UNIT_ASSIGNED_CONTEXT ( ( #26485, #9696, #18320 ) ) REPRESENTATION_CONTEXT ( 'NONE', 'WORKASPACE' ) );
#16635=CARTESIAN_POINT ( 'NONE',  ( 340.3127869742386338, 101.4626071723496779, -152.5098566583459672 ) ) ;
#16647=CIRCLE ( 'NONE', #4691, 6.000000000000005329 ) ;
#16711=CARTESIAN_POINT ( 'NONE',  ( 160.9807621135329612, 204.9999999999998863, -151.0000000000000284 ) ) ;
#16744=EDGE_CURVE ( 'NONE', #28048, #3815, #7903, .T. ) ;
#16748=ADVANCED_FACE ( 'NONE', ( #11956 ), #13545, .T. ) ;
#16760=DIRECTION ( 'NONE',  ( 0.000000000000000000, 0.000000000000000000, -1.000000000000000000 ) ) ;
#16791=CARTESIAN_POINT ( 'NONE',  ( 106.5441062369885117, 210.4993626438576086, -144.6099047286054713 ) ) ;
#16799=ORIENTED_EDGE ( 'NONE', *, *, #14791, .F. ) ;
#16815=CARTESIAN_POINT ( 'NONE',  ( 112.3311635761228899, 200.3498790610213973, -143.0657854549350816 ) ) ;
#16860=DIRECTION ( 'NONE',  ( -1.000000000000000000, 0.000000000000000000, 0.000000000000000000 ) ) ;
#16863=DIRECTION ( 'NONE',  ( 0.000000000000000000, 0.000000000000000000, -1.000000000000000000 ) ) ;
#16884=DIRECTION ( 'NONE',  ( -9.875160952879181910E-17, 0.000000000000000000, -1.000000000000000000 ) ) ;
#16916=CARTESIAN_POINT ( 'NONE',  ( 129.0384544366281716, 249.4018031322194702, -145.7833319456713639 ) ) ;
#16919=CARTESIAN_POINT ( 'NONE',  ( 145.7188177565814158, 467.1080826427131001, -145.0000000000000000 ) ) ;
#16953=CARTESIAN_POINT ( 'NONE',  ( 111.7339150226400619, 201.0596247756230355, -141.3391815462163663 ) ) ;
#16968=ORIENTED_EDGE ( 'NONE', *, *, #5394, .T. ) ;
#16983=CARTESIAN_POINT ( 'NONE',  ( 163.3555207136468539, 210.2026635890346711, -146.9347961558894156 ) ) ;
#16987=LINE ( 'NONE', #6636, #24353 ) ;
#17031=CARTESIAN_POINT ( 'NONE',  ( -140.1240808061633345, 61.15703788601678781, -145.0000000000000000 ) ) ;
#17056=CARTESIAN_POINT ( 'NONE',  ( 133.4364168238970194, 249.9598208048105903, -150.7960377432352175 ) ) ;
#17084=DIRECTION ( 'NONE',  ( 0.000000000000000000, 0.000000000000000000, 1.000000000000000000 ) ) ;
#17107=ORIENTED_EDGE ( 'NONE', *, *, #4414, .F. ) ;
#17113=ORIENTED_EDGE ( 'NONE', *, *, #4957, .F. ) ;
#17130=FACE_OUTER_BOUND ( 'NONE', #27960, .T. ) ;
#17140=EDGE_LOOP ( 'NONE', ( #14187, #3957, #8658, #10268 ) ) ;
#17162=DIRECTION ( 'NONE',  ( 0.000000000000000000, 0.000000000000000000, -1.000000000000000000 ) ) ;
#17165=CARTESIAN_POINT ( 'NONE',  ( 134.9999999999998579, 455.5353319318992362, -145.0000000000000000 ) ) ;
#17171=ADVANCED_FACE ( 'NONE', ( #10738 ), #22357, .T. ) ;
#17175=CARTESIAN_POINT ( 'NONE',  ( 349.0018770490532916, 96.44595867864244099, -155.7188177565815863 ) ) ;
#17177=DIRECTION ( 'NONE',  ( 0.8660254037844432595, 0.4999999999999919509, -0.000000000000000000 ) ) ;
#17199=CARTESIAN_POINT ( 'NONE',  ( 129.7957637945470708, 249.5459717953527274, -141.9885977063033522 ) ) ;
#17215=ORIENTED_EDGE ( 'NONE', *, *, #20537, .T. ) ;
#17224=VECTOR ( 'NONE', #23955, 1000.000000000000000 ) ;
#17228=CIRCLE ( 'NONE', #8527, 7.999999999999979572 ) ;
#17270=ORIENTED_EDGE ( 'NONE', *, *, #18850, .F. ) ;
#17343=CYLINDRICAL_SURFACE ( 'NONE', #12398, 10.00000000000000888 ) ;
#17394=EDGE_CURVE ( 'NONE', #19844, #1242, #13794, .T. ) ;
#17397=VERTEX_POINT ( 'NONE', #12162 ) ;
#17434=FACE_OUTER_BOUND ( 'NONE', #7215, .T. ) ;
#17457=ORIENTED_EDGE ( 'NONE', *, *, #14581, .T. ) ;
#17463=AXIS2_PLACEMENT_3D ( 'NONE', #24667, #11614, #23315 ) ;
#17482=CIRCLE ( 'NONE', #7412, 7.999999999999979572 ) ;
#17485=CARTESIAN_POINT ( 'NONE',  ( 107.2641058044744682, 208.5632379335606004, -140.4781857268138765 ) ) ;
#17495=DIRECTION ( 'NONE',  ( -0.000000000000000000, -1.000000000000000000, -0.000000000000000000 ) ) ;
#17510=AXIS2_PLACEMENT_3D ( 'NONE', #14423, #14989, #23736 ) ;
#17542=CARTESIAN_POINT ( 'NONE',  ( 158.7697712239360044, 201.6949277321624550, -149.5176478624189826 ) ) ;
#17557=VERTEX_POINT ( 'NONE', #6698 ) ;
#17579=DIRECTION ( 'NONE',  ( -1.000000000000000000, 0.000000000000000000, 0.000000000000000000 ) ) ;
#17582=ORIENTED_EDGE ( 'NONE', *, *, #1414, .F. ) ;
#17612=B_SPLINE_CURVE_WITH_KNOTS ( 'NONE', 3,
 ( #26, #4604, #6485, #19702, #15267, #19984, #24022, #8784, #4327, #6633, #17542, #15691, #26303, #13117, #15408, #24163, #13250, #21997, #13390, #2449, #22142, #2304, #21571, #17830, #21719, #11086, #19843, #8930, #1884, #10662, #166, #17689, #26437, #6765, #15546, #24295, #19420, #11234, #28167, #9072, #2032, #26583, #8507, #26018 ),
 .UNSPECIFIED., .F., .F.,
 ( 4, 2, 2, 2, 2, 2, 2, 2, 2, 2, 2, 2, 2, 2, 2, 2, 2, 2, 2, 2, 2, 4 ),
 ( 2.775557561562891351E-17, 0.001175389346958584033, 0.001763084020437862172, 0.002350778693917140311, 0.003526168040875716971, 0.004701557387834292764, 0.005876946734792868991, 0.007052336081751445218, 0.007640030755230769327, 0.008227725428710095171, 0.009403114775668663591, 0.01057850412262723375, 0.01175389346958580217, 0.01234158814306504995, 0.01292928281654429599, 0.01410467216350275860, 0.01528006151046121947, 0.01586775618394042908, 0.01645545085741964217, 0.01763084020437801977, 0.01821853487785717735, 0.01880622955133633145 ),
 .UNSPECIFIED. ) ;
#17640=CIRCLE ( 'NONE', #23137, 35.18636678425507114 ) ;
#17663=CIRCLE ( 'NONE', #5282, 35.18636678425505693 ) ;
#17664=ORIENTED_EDGE ( 'NONE', *, *, #26599, .T. ) ;
#17689=CARTESIAN_POINT ( 'NONE',  ( 158.7724735843374333, 201.6983920632174829, -140.4781857268138765 ) ) ;
#17720=CARTESIAN_POINT ( 'NONE',  ( 134.9999999999998579, 433.5940952139197293, -145.0000000000000000 ) ) ;
#17725=EDGE_LOOP ( 'NONE', ( #15825, #18982, #17113, #24853 ) ) ;
#17735=CARTESIAN_POINT ( 'NONE',  ( 140.9615602964835261, 249.4018026332753095, -145.7848141779618913 ) ) ;
#17742=FACE_OUTER_BOUND ( 'NONE', #17725, .T. ) ;
#17789=TOROIDAL_SURFACE ( 'NONE', #6773, 7.509856658345970715, 10.53396790234564762 ) ;
#17830=CARTESIAN_POINT ( 'NONE',  ( 157.5858673906874685, 200.2545008562565556, -143.4408232581956497 ) ) ;
#17887=AXIS2_PLACEMENT_3D ( 'NONE', #19910, #15766, #9000 ) ;
#17894=ORIENTED_EDGE ( 'NONE', *, *, #16744, .F. ) ;
#17930=VERTEX_POINT ( 'NONE', #21326 ) ;
#17933=CARTESIAN_POINT ( 'NONE',  ( -24.92338318254762441, 127.6681916698425567, -152.9999999999999432 ) ) ;
#17945=DIRECTION ( 'NONE',  ( 0.8660254037844432595, 0.4999999999999919509, -0.000000000000000000 ) ) ;
#17958=VERTEX_POINT ( 'NONE', #21607 ) ;
#17984=EDGE_CURVE ( 'NONE', #15093, #11335, #27532, .T. ) ;
#18003=DIRECTION ( 'NONE',  ( -0.8660254037844362651, 0.5000000000000039968, -0.000000000000000000 ) ) ;
#18013=CARTESIAN_POINT ( 'NONE',  ( 294.9233831825460470, 127.6681916698403398, -151.0000000000000284 ) ) ;
#18015=EDGE_CURVE ( 'NONE', #11276, #1877, #22516, .T. ) ;
#18019=CIRCLE ( 'NONE', #23532, 10.00000000000000888 ) ;
#18046=ORIENTED_EDGE ( 'NONE', *, *, #9711, .F. ) ;
#18064=AXIS2_PLACEMENT_3D ( 'NONE', #13246, #21717, #11082 ) ;
#18109=VERTEX_POINT ( 'NONE', #22614 ) ;
#18131=DIRECTION ( 'NONE',  ( 0.000000000000000000, 0.000000000000000000, -1.000000000000000000 ) ) ;
#18167=CARTESIAN_POINT ( 'NONE',  ( 134.9999999999998579, 220.0000000000000284, -169.9999999999999716 ) ) ;
#18177=CARTESIAN_POINT ( 'NONE',  ( 137.4797360180455144, 249.8978926453951885, -139.5328759577092228 ) ) ;
#18212=DIRECTION ( 'NONE',  ( 1.000000000000000000, 0.000000000000000000, 0.000000000000000000 ) ) ;
#18223=ORIENTED_EDGE ( 'NONE', *, *, #1722, .T. ) ;
#18275=ADVANCED_FACE ( 'NONE', ( #14417 ), #15650, .T. ) ;
#18286=ORIENTED_EDGE ( 'NONE', *, *, #3117, .T. ) ;
#18305=ORIENTED_EDGE ( 'NONE', *, *, #24535, .T. ) ;
#18320=( NAMED_UNIT ( * ) SI_UNIT ( $, .STERADIAN. ) SOLID_ANGLE_UNIT ( ) );
#18326=AXIS2_PLACEMENT_3D ( 'NONE', #1920, #6380, #6522 ) ;
#18357=AXIS2_PLACEMENT_3D ( 'NONE', #11820, #27026, #20134 ) ;
#18360=ORIENTED_EDGE ( 'NONE', *, *, #25671, .T. ) ;
#18421=DIRECTION ( 'NONE',  ( 0.000000000000000000, 0.000000000000000000, -1.000000000000000000 ) ) ;
#18442=CARTESIAN_POINT ( 'NONE',  ( 162.4217010148293525, 207.8312982882352173, -139.9035143180224736 ) ) ;
#18468=ORIENTED_EDGE ( 'NONE', *, *, #15362, .F. ) ;
#18477=AXIS2_PLACEMENT_3D ( 'NONE', #3635, #12844, #16863 ) ;
#18515=VECTOR ( 'NONE', #4649, 1000.000000000000000 ) ;
#18521=CARTESIAN_POINT ( 'NONE',  ( 164.9999999999998579, 220.0000000000000284, -122.9999999999999574 ) ) ;
#18538=ADVANCED_FACE ( 'NONE', ( #14350 ), #23109, .T. ) ;
#18547=CARTESIAN_POINT ( 'NONE',  ( 110.7507446791215102, 202.3364611620586402, -139.9035143180225020 ) ) ;
#18576=DIRECTION ( 'NONE',  ( 0.000000000000000000, 0.000000000000000000, 1.000000000000000000 ) ) ;
#18589=CARTESIAN_POINT ( 'NONE',  ( 410.1240808061609187, 61.15703788601284430, -145.0000000000000000 ) ) ;
#18604=VECTOR ( 'NONE', #10697, 999.9999999999998863 ) ;
#18618=CARTESIAN_POINT ( 'NONE',  ( 134.9999999999998579, 220.0000000000000284, -169.9999999999999716 ) ) ;
#18628=CIRCLE ( 'NONE', #13596, 10.71881775658151170 ) ;
#18655=VERTEX_POINT ( 'NONE', #16919 ) ;
#18681=ADVANCED_FACE ( 'NONE', ( #23814, #21505 ), #8157, .T. ) ;
#18682=CARTESIAN_POINT ( 'NONE',  ( 110.6543292814727550, 202.4672421913198264, -150.2048413890044003 ) ) ;
#18683=DIRECTION ( 'NONE',  ( 0.000000000000000000, 0.000000000000000000, -1.000000000000000000 ) ) ;
#18774=ORIENTED_EDGE ( 'NONE', *, *, #4077, .T. ) ;
#18778=ORIENTED_EDGE ( 'NONE', *, *, #1378, .T. ) ;
#18789=DIRECTION ( 'NONE',  ( 0.000000000000000000, 0.000000000000000000, -1.000000000000000000 ) ) ;
#18793=CARTESIAN_POINT ( 'NONE',  ( 144.9999999999998863, 220.0000000000000284, 109.9999999999999858 ) ) ;
#18823=CARTESIAN_POINT ( 'NONE',  ( 134.9999999999998579, 455.5353319318992362, -162.9307281190808681 ) ) ;
#18850=EDGE_CURVE ( 'NONE', #19026, #17930, #13850, .T. ) ;
#18856=CARTESIAN_POINT ( 'NONE',  ( 161.6393910565651026, 206.2021604053517763, -150.8447356795924179 ) ) ;
#18866=DIRECTION ( 'NONE',  ( 0.000000000000000000, 0.000000000000000000, -1.000000000000000000 ) ) ;
#18940=CARTESIAN_POINT ( 'NONE',  ( 106.6069624357703134, 210.3128146450298743, -143.4408232581956213 ) ) ;
#18959=AXIS2_PLACEMENT_3D ( 'NONE', #10748, #21370, #10886 ) ;
#18965=CARTESIAN_POINT ( 'NONE',  ( 109.4170858023077244, 204.3262714183213689, -139.0380470571626859 ) ) ;
#18982=ORIENTED_EDGE ( 'NONE', *, *, #23762, .T. ) ;
#19026=VERTEX_POINT ( 'NONE', #25777 ) ;
#19040=CARTESIAN_POINT ( 'NONE',  ( -70.31278697424053803, 101.4626071723526195, -145.0000000000000000 ) ) ;
#19071=CARTESIAN_POINT ( 'NONE',  ( 131.0301686624949014, 249.7374833449995322, -149.5158039499305573 ) ) ;
#19081=CARTESIAN_POINT ( 'NONE',  ( 109.0192378864665557, 205.0000000000002842, -151.0000000000000284 ) ) ;
#19098=AXIS2_PLACEMENT_3D ( 'NONE', #11462, #13906, #11608 ) ;
#19126=EDGE_LOOP ( 'NONE', ( #24110, #18223, #4934, #10043 ) ) ;
#19136=CARTESIAN_POINT ( 'NONE',  ( 161.1794673982064694, 205.3441676487868506, -151.0000000000000000 ) ) ;
#19165=CIRCLE ( 'NONE', #23311, 10.71881775658151170 ) ;
#19188=FACE_OUTER_BOUND ( 'NONE', #16031, .T. ) ;
#19189=ORIENTED_EDGE ( 'NONE', *, *, #4414, .T. ) ;
#19196=ORIENTED_EDGE ( 'NONE', *, *, #3155, .T. ) ;
#19217=CYLINDRICAL_SURFACE ( 'NONE', #3822, 30.00000000000000000 ) ;
#19224=VERTEX_POINT ( 'NONE', #2204 ) ;
#19227=ORIENTED_EDGE ( 'NONE', *, *, #21711, .F. ) ;
#19249=CARTESIAN_POINT ( 'NONE',  ( 124.9999999999998579, 220.0000000000000284, -119.9999999999999858 ) ) ;
#19279=DIRECTION ( 'NONE',  ( -1.000000000000000000, 0.000000000000000000, 0.000000000000000000 ) ) ;
#19315=FACE_OUTER_BOUND ( 'NONE', #13177, .T. ) ;
#19324=DIRECTION ( 'NONE',  ( 0.8660254037844432595, 0.4999999999999919509, -0.000000000000000000 ) ) ;
#19352=CARTESIAN_POINT ( 'NONE',  ( 131.3319829069345417, 249.7767514970616674, -149.7646631383025237 ) ) ;
#19358=FACE_OUTER_BOUND ( 'NONE', #13886, .T. ) ;
#19420=CARTESIAN_POINT ( 'NONE',  ( 159.6524665415090283, 202.9035392909954965, -139.5328759577091375 ) ) ;
#19447=ORIENTED_EDGE ( 'NONE', *, *, #20319, .T. ) ;
#19474=ORIENTED_EDGE ( 'NONE', *, *, #678, .F. ) ;
#19479=DIRECTION ( 'NONE',  ( 0.4999999999999920064, -0.8660254037844432595, 0.000000000000000000 ) ) ;
#19502=DIRECTION ( 'NONE',  ( 0.000000000000000000, 0.000000000000000000, 1.000000000000000000 ) ) ;
#19504=ADVANCED_FACE ( 'NONE', ( #17130, #25741 ), #4046, .T. ) ;
#19505=CYLINDRICAL_SURFACE ( 'NONE', #21541, 6.000000000000032863 ) ;
#19508=CARTESIAN_POINT ( 'NONE',  ( 106.9648806875826068, 209.3191036920025283, -148.6640466283485580 ) ) ;
#19579=( NAMED_UNIT ( * ) PLANE_ANGLE_UNIT ( ) SI_UNIT ( $, .RADIAN. ) );
#19606=AXIS2_PLACEMENT_3D ( 'NONE', #20150, #18003, #21134 ) ;
#19647=CYLINDRICAL_SURFACE ( 'NONE', #26816, 30.00000000000000000 ) ;
#19661=CIRCLE ( 'NONE', #28352, 562.1290781602208426 ) ;
#19680=ORIENTED_EDGE ( 'NONE', *, *, #1284, .F. ) ;
#19701=DIRECTION ( 'NONE',  ( 0.000000000000000000, 1.000000000000000000, 0.000000000000000000 ) ) ;
#19702=CARTESIAN_POINT ( 'NONE',  ( 160.2722134808911107, 203.8336097610383035, -150.8460904732142751 ) ) ;
#19734=DIRECTION ( 'NONE',  ( 1.000000000000000000, 0.000000000000000000, 0.000000000000000000 ) ) ;
#19777=ORIENTED_EDGE ( 'NONE', *, *, #14454, .F. ) ;
#19825=ORIENTED_EDGE ( 'NONE', *, *, #2013, .T. ) ;
#19836=CARTESIAN_POINT ( 'NONE',  ( 134.9999999999998579, 244.8793018922092699, -151.0000000000000284 ) ) ;
#19843=CARTESIAN_POINT ( 'NONE',  ( 157.8683049041797517, 200.5822371829430040, -142.3407963099403446 ) ) ;
#19844=VERTEX_POINT ( 'NONE', #18823 ) ;
#19853=AXIS2_PLACEMENT_3D ( 'NONE', #15172, #9904, #2076 ) ;
#19910=CARTESIAN_POINT ( 'NONE',  ( 134.9999999999998579, 457.0747856552986832, -152.5098566583459672 ) ) ;
#19953=DIRECTION ( 'NONE',  ( -0.5000000000000039968, -0.8660254037844362651, -1.224646799147353454E-16 ) ) ;
#19984=CARTESIAN_POINT ( 'NONE',  ( 159.9611678081874402, 203.3574085914958118, -150.6837522856751264 ) ) ;
#19986=ORIENTED_EDGE ( 'NONE', *, *, #13349, .F. ) ;
#19994=AXIS2_PLACEMENT_3D ( 'NONE', #893, #9666, #18421 ) ;
#20045=VERTEX_POINT ( 'NONE', #9048 ) ;
#20119=LINE ( 'NONE', #19836, #10057 ) ;
#20134=DIRECTION ( 'NONE',  ( 0.000000000000000000, 0.000000000000000000, -1.000000000000000000 ) ) ;
#20150=CARTESIAN_POINT ( 'NONE',  ( 294.9233831825460470, 127.6681916698403398, -145.0000000000000000 ) ) ;
#20164=CARTESIAN_POINT ( 'NONE',  ( 161.8967505429097287, 206.7072948235298782, -139.3076717160242595 ) ) ;
#20177=CARTESIAN_POINT ( 'NONE',  ( 138.0067716801852669, 249.8494523599397894, -139.8040206391607967 ) ) ;
#20263=EDGE_CURVE ( 'NONE', #5588, #20045, #25822, .T. ) ;
#20274=MECHANICAL_DESIGN_GEOMETRIC_PRESENTATION_REPRESENTATION('',(#95),#16616);
#20280=ORIENTED_EDGE ( 'NONE', *, *, #5164, .T. ) ;
#20283=EDGE_CURVE ( 'NONE', #7328, #21528, #13453, .T. ) ;
#20306=CARTESIAN_POINT ( 'NONE',  ( 160.9807621135329612, 204.9999999999999147, -138.9999999999999432 ) ) ;
#20319=EDGE_CURVE ( 'NONE', #17958, #9931, #5622, .T. ) ;
#20352=ORIENTED_EDGE ( 'NONE', *, *, #16744, .T. ) ;
#20361=CIRCLE ( 'NONE', #24956, 10.53396790234564406 ) ;
#20363=PRODUCT_DEFINITION ( 'UNKNOWN', '', #12944, #23839 ) ;
#20371=CONICAL_SURFACE ( 'NONE', #24043, 30.00000000000001421, 0.7853981633974500554 ) ;
#20379=EDGE_CURVE ( 'NONE', #11335, #15093, #18019, .T. ) ;
#20411=CARTESIAN_POINT ( 'NONE',  ( 134.9999999999998579, 220.0000000000000284, -122.9999999999999574 ) ) ;
#20455=ORIENTED_EDGE ( 'NONE', *, *, #7697, .T. ) ;
#20527=DIRECTION ( 'NONE',  ( -0.000000000000000000, -1.000000000000000000, -0.000000000000000000 ) ) ;
#20537=EDGE_CURVE ( 'NONE', #23894, #26741, #13585, .T. ) ;
#20571=VERTEX_POINT ( 'NONE', #9266 ) ;
#20579=ORIENTED_EDGE ( 'NONE', *, *, #3155, .F. ) ;
#20581=CIRCLE ( 'NONE', #26537, 17.93072811908088937 ) ;
#20591=CARTESIAN_POINT ( 'NONE',  ( 161.1767780239350145, 205.3395095159081336, -138.9999999999999432 ) ) ;
#20613=EDGE_LOOP ( 'NONE', ( #4806, #8317, #409, #14610 ) ) ;
#20642=ADVANCED_FACE ( 'NONE', ( #9414 ), #24472, .T. ) ;
#20660=AXIS2_PLACEMENT_3D ( 'NONE', #8819, #59, #17579 ) ;
#20681=CARTESIAN_POINT ( 'NONE',  ( -79.00187704905532371, 96.44595867864549632, -155.7188177565815579 ) ) ;
#20693=CARTESIAN_POINT ( 'NONE',  ( 110.4531970035855579, 202.7493367244436513, -150.3892986974657617 ) ) ;
#20739=CARTESIAN_POINT ( 'NONE',  ( 135.1960665634829581, 250.0000000000000568, -138.9999999999999432 ) ) ;
#20824=EDGE_LOOP ( 'NONE', ( #1310, #20280, #24791, #3856 ) ) ;
#20913=DIRECTION ( 'NONE',  ( -1.000000000000000000, 0.000000000000000000, 0.000000000000000000 ) ) ;
#20944=CARTESIAN_POINT ( 'NONE',  ( -24.92338318254761020, 127.6681916698425567, -145.0000000000000000 ) ) ;
#20977=CARTESIAN_POINT ( 'NONE',  ( 156.5461074670752453, 207.5603490538953224, -145.0000000000000000 ) ) ;
#21004=CARTESIAN_POINT ( 'NONE',  ( 163.0331409777209331, 209.3154830203752397, -148.6534330424975963 ) ) ;
#21034=PRODUCT_DEFINITION_SHAPE ( 'NONE', 'NONE',  #20363 ) ;
#21057=CARTESIAN_POINT ( 'NONE',  ( -140.1240808061633345, 61.15703788601678781, 393.1631314933625845 ) ) ;
#21067=VERTEX_POINT ( 'NONE', #3122 ) ;
#21073=CARTESIAN_POINT ( 'NONE',  ( 134.9999999999998579, 244.8793018922092699, -145.0000000000000000 ) ) ;
#21082=CARTESIAN_POINT ( 'NONE',  ( 134.2103424514737640, 249.9921085342972162, -150.9609010065648249 ) ) ;
#21091=CARTESIAN_POINT ( 'NONE',  ( 106.5442058163639985, 210.4990643932678438, -145.3948054049556902 ) ) ;
#21108=ADVANCED_FACE ( 'NONE', ( #27257 ), #16185, .T. ) ;
#21134=DIRECTION ( 'NONE',  ( 0.000000000000000000, 0.000000000000000000, -1.000000000000000000 ) ) ;
#21150=CARTESIAN_POINT ( 'NONE',  ( 163.3936278923558518, 210.3145496728149340, -146.5522648598509363 ) ) ;
#21233=CARTESIAN_POINT ( 'NONE',  ( 108.6319795274282143, 205.6865347771202721, -150.9608879355640170 ) ) ;
#21291=CARTESIAN_POINT ( 'NONE',  ( 163.2542326668747990, 209.9142827673095439, -147.6595947404202605 ) ) ;
#21308=CIRCLE ( 'NONE', #9387, 30.00000000000001421 ) ;
#21326=CARTESIAN_POINT ( 'NONE',  ( 114.7546517713170857, 220.0000000000000284, -189.9999999999999716 ) ) ;
#21331=CIRCLE ( 'NONE', #12192, 6.000000000000005329 ) ;
#21340=DIRECTION ( 'NONE',  ( 0.000000000000000000, 0.000000000000000000, -1.000000000000000000 ) ) ;
#21342=CARTESIAN_POINT ( 'NONE',  ( 156.5461074670752453, 207.5603490538953224, -151.0000000000000284 ) ) ;
#21345=ORIENTED_EDGE ( 'NONE', *, *, #21603, .T. ) ;
#21364=CARTESIAN_POINT ( 'NONE',  ( 130.1183073479271002, 249.6003596541303011, -148.4939404368777218 ) ) ;
#21370=DIRECTION ( 'NONE',  ( 0.000000000000000000, 0.000000000000000000, -1.000000000000000000 ) ) ;
#21376=CARTESIAN_POINT ( 'NONE',  ( 108.8204812537424715, 205.3442565862195863, -150.9999999999999716 ) ) ;
#21411=ORIENTED_EDGE ( 'NONE', *, *, #14530, .F. ) ;
#21488=ORIENTED_EDGE ( 'NONE', *, *, #21603, .F. ) ;
#21502=PRODUCT ( 'Rotating Grip', 'Rotating Grip', '', ( #21845 ) ) ;
#21503=CARTESIAN_POINT ( 'NONE',  ( 129.6110901909775635, 249.5124271981383401, -142.3325995572698446 ) ) ;
#21505=FACE_BOUND ( 'NONE', #4950, .T. ) ;
#21506=CARTESIAN_POINT ( 'NONE',  ( 160.9807621135329612, 204.9999999999998863, -151.0000000000000284 ) ) ;
#21525=AXIS2_PLACEMENT_3D ( 'NONE', #15238, #9046, #6458 ) ;
#21526=EDGE_LOOP ( 'NONE', ( #17270, #15360, #25348, #21488 ) ) ;
#21528=VERTEX_POINT ( 'NONE', #17933 ) ;
#21541=AXIS2_PLACEMENT_3D ( 'NONE', #8593, #11171, #28382 ) ;
#21571=CARTESIAN_POINT ( 'NONE',  ( 157.4823930684554512, 200.1367640063166391, -144.2111520032349006 ) ) ;
#21603=EDGE_CURVE ( 'NONE', #17930, #13771, #24543, .T. ) ;
#21604=CYLINDRICAL_SURFACE ( 'NONE', #8059, 6.000000000000032863 ) ;
#21607=CARTESIAN_POINT ( 'NONE',  ( 107.9999999999998437, 220.0000000000000284, -119.9999999999999858 ) ) ;
#21608=DIRECTION ( 'NONE',  ( 1.000000000000000000, 0.000000000000000000, 0.000000000000000000 ) ) ;
#21612=EDGE_CURVE ( 'NONE', #23894, #16059, #16647, .T. ) ;
#21650=CARTESIAN_POINT ( 'NONE',  ( 129.0001992662464829, 249.3939175884451629, -144.6008566625276615 ) ) ;
#21660=CARTESIAN_POINT ( 'NONE',  ( 108.1065091513366809, 206.7042902742356887, -150.6837522856750411 ) ) ;
#21681=LINE ( 'NONE', #12931, #24798 ) ;
#21711=EDGE_CURVE ( 'NONE', #13229, #23466, #23981, .T. ) ;
#21717=DIRECTION ( 'NONE',  ( -0.000000000000000000, -0.000000000000000000, 1.000000000000000000 ) ) ;
#21719=CARTESIAN_POINT ( 'NONE',  ( 157.6621827647630880, 200.3416932910694470, -143.0663072493378820 ) ) ;
#21735=DIRECTION ( 'NONE',  ( -1.224646799147353207E-16, 0.000000000000000000, -1.000000000000000000 ) ) ;
#21745=ADVANCED_FACE ( 'NONE', ( #5987 ), #26267, .T. ) ;
#21759=CARTESIAN_POINT ( 'NONE',  ( 134.9999999999998579, 433.5940952139197293, -145.0000000000000000 ) ) ;
#21765=DIRECTION ( 'NONE',  ( 0.000000000000000000, 0.000000000000000000, -1.000000000000000000 ) ) ;
#21772=CARTESIAN_POINT ( 'NONE',  ( 294.9233831825460470, 127.6681916698403398, -138.9999999999999432 ) ) ;
#21779=DIRECTION ( 'NONE',  ( 0.000000000000000000, -0.000000000000000000, -1.000000000000000000 ) ) ;
#21784=EDGE_LOOP ( 'NONE', ( #20455, #12747 ) ) ;
#21798=CARTESIAN_POINT ( 'NONE',  ( 113.4538925329242574, 207.5603490538955782, -138.9999999999999432 ) ) ;
#21799=DIRECTION ( 'NONE',  ( 0.8660254037844432595, 0.4999999999999919509, 0.000000000000000000 ) ) ;
#21805=FACE_OUTER_BOUND ( 'NONE', #22774, .T. ) ;
#21836=CARTESIAN_POINT ( 'NONE',  ( 109.7310248654090117, 203.8285304009907293, -150.8447356795924179 ) ) ;
#21845=PRODUCT_CONTEXT ( 'NONE', #1202, 'mechanical' ) ;
#21864=CARTESIAN_POINT ( 'NONE',  ( -140.1240808061633061, 61.15703788601673097, -683.1631314933625845 ) ) ;
#21882=AXIS2_PLACEMENT_3D ( 'NONE', #21073, #27666, #14615 ) ;
#21893=DIRECTION ( 'NONE',  ( 0.000000000000000000, -0.000000000000000000, 1.000000000000000000 ) ) ;
#21935=CARTESIAN_POINT ( 'NONE',  ( 134.9999999999998863, 537.6859242279716682, 393.1631314933625845 ) ) ;
#21985=ORIENTED_EDGE ( 'NONE', *, *, #7549, .F. ) ;
#21997=CARTESIAN_POINT ( 'NONE',  ( 157.5925105526923744, 200.2621716282842499, -146.5591841905931290 ) ) ;
#22030=ADVANCED_FACE ( 'NONE', ( #10274 ), #23085, .T. ) ;
#22063=ORIENTED_EDGE ( 'NONE', *, *, #15621, .T. ) ;
#22074=AXIS2_PLACEMENT_3D ( 'NONE', #16370, #12204, #12061 ) ;
#22081=CARTESIAN_POINT ( 'NONE',  ( -24.92338318254763152, 127.6681916698425567, -137.0000000000000568 ) ) ;
#22085=CARTESIAN_POINT ( 'NONE',  ( 107.5773805851584939, 207.8333816969443433, -139.9049692442121398 ) ) ;
#22133=EDGE_CURVE ( 'NONE', #28048, #17557, #51, .T. ) ;
#22142=CARTESIAN_POINT ( 'NONE',  ( 157.4559486869681848, 200.1070271554761462, -145.3948054049556902 ) ) ;
#22193=CARTESIAN_POINT ( 'NONE',  ( 140.6165658301760004, 249.4696452662898025, -147.1195141158909223 ) ) ;
#22243=DIRECTION ( 'NONE',  ( 0.000000000000000000, 0.000000000000000000, -1.000000000000000000 ) ) ;
#22336=CARTESIAN_POINT ( 'NONE',  ( 137.6643377305021261, 249.8836732857602669, -150.3903514073973611 ) ) ;
#22357=CYLINDRICAL_SURFACE ( 'NONE', #12412, 6.000000000000032863 ) ;
#22359=CLOSED_SHELL ( 'NONE', ( #23895, #8664, #11939, #24925, #1846, #8709, #15037, #11412, #6142, #21108, #22030, #14124, #168, #5133, #11515, #2878, #6155, #26249, #12881, #23934, #24502, #16748, #18538, #4025, #18275, #5872, #19504, #7711, #7379, #4614, #20642, #10601, #17171, #9698, #21745, #8382, #18681, #23387 ) ) ;
#22396=CIRCLE ( 'NONE', #4059, 562.1290781602206152 ) ;
#22436=DIRECTION ( 'NONE',  ( -0.8660254037844362651, 0.5000000000000039968, -0.000000000000000000 ) ) ;
#22482=ORIENTED_EDGE ( 'NONE', *, *, #3800, .F. ) ;
#22503=DIRECTION ( 'NONE',  ( 0.000000000000000000, 0.000000000000000000, -1.000000000000000000 ) ) ;
#22511=DIRECTION ( 'NONE',  ( 0.000000000000000000, 0.000000000000000000, -1.000000000000000000 ) ) ;
#22516=CIRCLE ( 'NONE', #20660, 30.00000000000001421 ) ;
#22563=DIRECTION ( 'NONE',  ( -0.8660254037844363761, 0.5000000000000039968, -0.000000000000000000 ) ) ;
#22610=DIRECTION ( 'NONE',  ( 0.8660254037844432595, 0.4999999999999918954, 0.000000000000000000 ) ) ;
#22614=CARTESIAN_POINT ( 'NONE',  ( 144.9999999999998863, 220.0000000000000284, -119.9999999999999858 ) ) ;
#22618=EDGE_CURVE ( 'NONE', #9931, #17958, #22660, .T. ) ;
#22630=CARTESIAN_POINT ( 'NONE',  ( 139.5196418751131091, 249.6589030830498075, -148.9655004847909936 ) ) ;
#22632=CARTESIAN_POINT ( 'NONE',  ( 134.9999999999998863, 250.0000000000000568, -151.0000000000000284 ) ) ;
#22660=CIRCLE ( 'NONE', #18064, 27.00000000000002487 ) ;
#22699=AXIS2_PLACEMENT_3D ( 'NONE', #5640, #18576, #772 ) ;
#22749=AXIS2_PLACEMENT_3D ( 'NONE', #25111, #16088, #5149 ) ;
#22774=EDGE_LOOP ( 'NONE', ( #15757, #18468, #4027, #13111 ) ) ;
#22780=DIRECTION ( 'NONE',  ( 0.5000000000000039968, 0.8660254037844362651, 0.000000000000000000 ) ) ;
#22860=ORIENTED_EDGE ( 'NONE', *, *, #25330, .T. ) ;
#22878=ORIENTED_EDGE ( 'NONE', *, *, #23525, .F. ) ;
#22907=EDGE_LOOP ( 'NONE', ( #26902, #22063, #21411, #6160 ) ) ;
#22917=CARTESIAN_POINT ( 'NONE',  ( 410.1240808061609187, 61.15703788601284430, 393.1631314933625845 ) ) ;
#22978=ORIENTED_EDGE ( 'NONE', *, *, #7125, .T. ) ;
#22996=CARTESIAN_POINT ( 'NONE',  ( 110.1465075748078277, 203.1971239227096646, -150.6145052419835224 ) ) ;
#23061=VECTOR ( 'NONE', #9320, 1000.000000000000000 ) ;
#23066=VECTOR ( 'NONE', #27682, 999.9999999999998863 ) ;
#23085=TOROIDAL_SURFACE ( 'NONE', #613, 7.509856658345970715, 10.53396790234564762 ) ;
#23093=AXIS2_PLACEMENT_3D ( 'NONE', #113, #9164, #8878 ) ;
#23095=EDGE_LOOP ( 'NONE', ( #7793, #5928, #309, #27822 ) ) ;
#23102=DIRECTION ( 'NONE',  ( 0.000000000000000000, 0.000000000000000000, -1.000000000000000000 ) ) ;
#23109=CYLINDRICAL_SURFACE ( 'NONE', #22074, 6.000000000000032863 ) ;
#23116=CARTESIAN_POINT ( 'NONE',  ( -24.92338318254761020, 127.6681916698425567, -145.0000000000000000 ) ) ;
#23126=EDGE_LOOP ( 'NONE', ( #5531, #17215, #19986, #19474 ) ) ;
#23137=AXIS2_PLACEMENT_3D ( 'NONE', #24584, #8646, #19701 ) ;
#23140=CARTESIAN_POINT ( 'NONE',  ( 112.4153400233872162, 200.2531221032099609, -146.5522648598509647 ) ) ;
#23172=CARTESIAN_POINT ( 'NONE',  ( 163.2529665854376333, 209.9107191942472355, -142.3325995572698446 ) ) ;
#23176=AXIS2_PLACEMENT_3D ( 'NONE', #4818, #25079, #22503 ) ;
#23246=CARTESIAN_POINT ( 'NONE',  ( 129.3069818644945883, 249.4552694810368507, -146.9347961558894724 ) ) ;
#23309=CARTESIAN_POINT ( 'NONE',  ( 134.9999999999998579, 457.0747856552986832, -145.0000000000000000 ) ) ;
#23310=CARTESIAN_POINT ( 'NONE',  ( 163.4434812112566249, 210.4619483375885238, -145.7833319456713639 ) ) ;
#23311=AXIS2_PLACEMENT_3D ( 'NONE', #7318, #17945, #16093 ) ;
#23315=DIRECTION ( 'NONE',  ( 0.5000000000000039968, 0.8660254037844364872, 0.000000000000000000 ) ) ;
#23318=ORIENTED_EDGE ( 'NONE', *, *, #4957, .T. ) ;
#23349=CARTESIAN_POINT ( 'NONE',  ( 340.3127869742386338, 101.4626071723496779, -145.0000000000000000 ) ) ;
#23354=CARTESIAN_POINT ( 'NONE',  ( 134.9999999999998579, 404.6636166603179277, -151.0000000000000000 ) ) ;
#23381=CARTESIAN_POINT ( 'NONE',  ( 132.8750286730203811, 249.9251938516255791, -150.6145052419835508 ) ) ;
#23387=ADVANCED_FACE ( 'NONE', ( #15576 ), #20371, .T. ) ;
#23388=AXIS2_PLACEMENT_3D ( 'NONE', #24743, #13693, #751 ) ;
#23415=CARTESIAN_POINT ( 'NONE',  ( 112.1383963276659159, 200.5739753623955437, -147.6595947404202320 ) ) ;
#23432=VERTEX_POINT ( 'NONE', #9249 ) ;
#23449=CARTESIAN_POINT ( 'NONE',  ( 162.2129141269701620, 207.3671766611915359, -150.3892986974657617 ) ) ;
#23466=VERTEX_POINT ( 'NONE', #3055 ) ;
#23518=EDGE_CURVE ( 'NONE', #17397, #1528, #6173, .T. ) ;
#23525=EDGE_CURVE ( 'NONE', #3222, #5588, #13993, .T. ) ;
#23532=AXIS2_PLACEMENT_3D ( 'NONE', #1656, #14222, #8558 ) ;
#23540=CIRCLE ( 'NONE', #23093, 17.93072811908088937 ) ;
#23561=CARTESIAN_POINT ( 'NONE',  ( 111.5720349012335646, 201.2611006861219494, -148.9571385985325094 ) ) ;
#23592=CARTESIAN_POINT ( 'NONE',  ( 134.9999999999998579, 433.5940952139197293, -145.0000000000000000 ) ) ;
#23633=DIRECTION ( 'NONE',  ( -0.8660254037844363761, 0.5000000000000041078, -0.000000000000000000 ) ) ;
#23714=VERTEX_POINT ( 'NONE', #6484 ) ;
#23728=AXIS2_PLACEMENT_3D ( 'NONE', #4422, #17495, #13347 ) ;
#23736=DIRECTION ( 'NONE',  ( 0.000000000000000000, 0.000000000000000000, -1.000000000000000000 ) ) ;
#23753=ORIENTED_EDGE ( 'NONE', *, *, #8470, .F. ) ;
#23762=EDGE_CURVE ( 'NONE', #17397, #23714, #17640, .T. ) ;
#23773=DIRECTION ( 'NONE',  ( 0.000000000000000000, 0.000000000000000000, -1.000000000000000000 ) ) ;
#23788=DIRECTION ( 'NONE',  ( -0.8660254037844363761, 0.5000000000000039968, -0.000000000000000000 ) ) ;
#23793=EDGE_CURVE ( 'NONE', #1877, #11276, #21308, .T. ) ;
#23797=ORIENTED_EDGE ( 'NONE', *, *, #20283, .F. ) ;
#23811=CARTESIAN_POINT ( 'NONE',  ( 132.5217165206440200, 249.8980084815856912, -139.5322470298331439 ) ) ;
#23814=FACE_OUTER_BOUND ( 'NONE', #25291, .T. ) ;
#23822=EDGE_CURVE ( 'NONE', #13520, #26295, #25427, .T. ) ;
#23839=PRODUCT_DEFINITION_CONTEXT ( 'detailed design', #2664, 'design' ) ;
#23867=CARTESIAN_POINT ( 'NONE',  ( 319.9779125536060178, 113.2029523930392969, -145.0000000000000000 ) ) ;
#23894=VERTEX_POINT ( 'NONE', #11809 ) ;
#23895=ADVANCED_FACE ( 'NONE', ( #14244 ), #13552, .T. ) ;
#23900=CARTESIAN_POINT ( 'NONE',  ( 354.3612859273441700, 105.7287271543778076, -145.0000000000000000 ) ) ;
#23908=CARTESIAN_POINT ( 'NONE',  ( 164.9999999999998579, 220.0000000000000284, -122.9999999999999574 ) ) ;
#23934=ADVANCED_FACE ( 'NONE', ( #5038, #9646 ), #5604, .F. ) ;
#23936=ORIENTED_EDGE ( 'NONE', *, *, #13349, .T. ) ;
#23955=DIRECTION ( 'NONE',  ( 0.8660254037844432595, 0.4999999999999919509, -0.000000000000000000 ) ) ;
#23964=CARTESIAN_POINT ( 'NONE',  ( 107.2624567859743792, 208.5673104118459378, -149.5176478624189542 ) ) ;
#23981=CIRCLE ( 'NONE', #27192, 10.53396790234563518 ) ;
#24005=AXIS2_PLACEMENT_3D ( 'NONE', #18589, #7677, #24781 ) ;
#24022=CARTESIAN_POINT ( 'NONE',  ( 159.8564679241521276, 203.2015132085163600, -150.6165463336312769 ) ) ;
#24030=TOROIDAL_SURFACE ( 'NONE', #7530, 7.509856658345970715, 10.53396790234564762 ) ;
#24043=AXIS2_PLACEMENT_3D ( 'NONE', #24055, #4358, #6662 ) ;
#24055=CARTESIAN_POINT ( 'NONE',  ( 134.9999999999998579, 220.0000000000000284, -122.9999999999999574 ) ) ;
#24110=ORIENTED_EDGE ( 'NONE', *, *, #22618, .F. ) ;
#24163=CARTESIAN_POINT ( 'NONE',  ( 157.7131785260345112, 200.4010886758948686, -147.1195141158909223 ) ) ;
#24241=CARTESIAN_POINT ( 'NONE',  ( 106.8486790052090782, 209.6310448320832904, -141.8266621613457517 ) ) ;
#24295=CARTESIAN_POINT ( 'NONE',  ( 159.5493656458986322, 202.7558958333859209, -139.6178255645964441 ) ) ;
#24296=CIRCLE ( 'NONE', #17887, 10.53396790234564762 ) ;
#24298=ORIENTED_EDGE ( 'NONE', *, *, #5358, .F. ) ;
#24311=CIRCLE ( 'NONE', #3679, 10.71881775658151170 ) ;
#24318=VERTEX_POINT ( 'NONE', #26848 ) ;
#24341=CARTESIAN_POINT ( 'NONE',  ( 136.3643978939877570, 249.9695740037962821, -150.8460904732142751 ) ) ;
#24353=VECTOR ( 'NONE', #12833, 1000.000000000000000 ) ;
#24390=CIRCLE ( 'NONE', #11106, 10.00000000000000888 ) ;
#24416=VERTEX_POINT ( 'NONE', #3412 ) ;
#24472=TOROIDAL_SURFACE ( 'NONE', #24005, -538.1631314933625845, 562.1290781602207289 ) ;
#24491=CARTESIAN_POINT ( 'NONE',  ( 135.7881857370864225, 249.9921081881951750, -150.9608879355639885 ) ) ;
#24502=ADVANCED_FACE ( 'NONE', ( #6423 ), #3436, .T. ) ;
#24511=CARTESIAN_POINT ( 'NONE',  ( 340.3127869742386338, 101.4626071723496779, -137.4901433416540328 ) ) ;
#24535=EDGE_CURVE ( 'NONE', #7370, #23432, #9006, .T. ) ;
#24543=LINE ( 'NONE', #10653, #23061 ) ;
#24556=CIRCLE ( 'NONE', #9900, 10.71881775658151170 ) ;
#24560=DIRECTION ( 'NONE',  ( 0.8660254037844432595, 0.4999999999999919509, -0.000000000000000000 ) ) ;
#24584=CARTESIAN_POINT ( 'NONE',  ( -49.97791255360778706, 113.2029523930418975, -145.0000000000000000 ) ) ;
#24589=CIRCLE ( 'NONE', #22749, 10.53396790234564762 ) ;
#24667=CARTESIAN_POINT ( 'NONE',  ( 319.9779125536060178, 113.2029523930392969, -145.0000000000000000 ) ) ;
#24672=CARTESIAN_POINT ( 'NONE',  ( 106.9638955565933145, 209.3217385430746447, -141.3400049877799916 ) ) ;
#24700=EDGE_CURVE ( 'NONE', #20571, #5309, #24556, .T. ) ;
#24722=CARTESIAN_POINT ( 'NONE',  ( 134.9999999999998579, 250.0000000000000568, -138.9999999999999432 ) ) ;
#24743=CARTESIAN_POINT ( 'NONE',  ( 134.9999999999998579, 220.0000000000000284, -189.9999999999999716 ) ) ;
#24781=DIRECTION ( 'NONE',  ( 0.000000000000000000, 0.000000000000000000, -1.000000000000000000 ) ) ;
#24791=ORIENTED_EDGE ( 'NONE', *, *, #13729, .F. ) ;
#24798=VECTOR ( 'NONE', #17084, 1000.000000000000000 ) ;
#24853=ORIENTED_EDGE ( 'NONE', *, *, #4629, .F. ) ;
#24881=DIRECTION ( 'NONE',  ( 0.000000000000000000, 0.000000000000000000, -1.000000000000000000 ) ) ;
#24925=ADVANCED_FACE ( 'NONE', ( #17742 ), #82, .T. ) ;
#24940=CARTESIAN_POINT ( 'NONE',  ( -73.64246817076464424, 87.16319020291010133, -145.0000000000000000 ) ) ;
#24956=AXIS2_PLACEMENT_3D ( 'NONE', #16338, #27646, #7708 ) ;
#24999=ORIENTED_EDGE ( 'NONE', *, *, #4629, .T. ) ;
#25043=DIRECTION ( 'NONE',  ( -0.8660254037844362651, 0.5000000000000039968, -0.000000000000000000 ) ) ;
#25065=CARTESIAN_POINT ( 'NONE',  ( 0.000000000000000000, 0.000000000000000000, 0.000000000000000000 ) ) ;
#25079=DIRECTION ( 'NONE',  ( -0.8660254037844362651, 0.5000000000000039968, -0.000000000000000000 ) ) ;
#25111=CARTESIAN_POINT ( 'NONE',  ( 134.9999999999998579, 457.0747856552986832, -137.4901433416540328 ) ) ;
#25145=CARTESIAN_POINT ( 'NONE',  ( 111.2314996473659647, 201.6932835404816160, -149.5158039499305573 ) ) ;
#25146=DIRECTION ( 'NONE',  ( -0.8660254037844363761, 0.5000000000000041078, -0.000000000000000000 ) ) ;
#25202=ORIENTED_EDGE ( 'NONE', *, *, #11814, .F. ) ;
#25246=DIRECTION ( 'NONE',  ( -0.8660254037844359321, 0.5000000000000045519, 0.000000000000000000 ) ) ;
#25275=DIRECTION ( 'NONE',  ( 0.000000000000000000, 0.000000000000000000, -1.000000000000000000 ) ) ;
#25287=CARTESIAN_POINT ( 'NONE',  ( 110.0434296560979135, 203.3505179757799795, -150.6809294437985898 ) ) ;
#25288=ADVANCED_BREP_SHAPE_REPRESENTATION ( '', ( #8854, #10637 ), #10190 ) ;
#25291=EDGE_LOOP ( 'NONE', ( #26378, #8632 ) ) ;
#25330=EDGE_CURVE ( 'NONE', #1070, #26295, #3934, .T. ) ;
#25343=DIRECTION ( 'NONE',  ( 1.000000000000000000, 0.000000000000000000, 0.000000000000000000 ) ) ;
#25348=ORIENTED_EDGE ( 'NONE', *, *, #15362, .T. ) ;
#25386=ORIENTED_EDGE ( 'NONE', *, *, #5164, .F. ) ;
#25427=CIRCLE ( 'NONE', #13069, 35.18636678425507114 ) ;
#25461=CARTESIAN_POINT ( 'NONE',  ( 161.7277574978466816, 206.3741923490296131, -150.7960377432351891 ) ) ;
#25533=CARTESIAN_POINT ( 'NONE',  ( 129.3169142913460234, 249.4568486868007540, -143.0657854549350532 ) ) ;
#25561=CARTESIAN_POINT ( 'NONE',  ( 112.4076948732478911, 200.2619365998405954, -143.4419542882358201 ) ) ;
#25593=CARTESIAN_POINT ( 'NONE',  ( 163.4557797152162095, 210.4990210588524064, -144.6008566625276615 ) ) ;
#25607=DIRECTION ( 'NONE',  ( 0.8660254037844432595, 0.4999999999999919509, -0.000000000000000000 ) ) ;
#25611=ORIENTED_EDGE ( 'NONE', *, *, #24535, .F. ) ;
#25623=AXIS2_PLACEMENT_3D ( 'NONE', #8295, #348, #12623 ) ;
#25671=EDGE_CURVE ( 'NONE', #13771, #1877, #11518, .T. ) ;
#25706=CARTESIAN_POINT ( 'NONE',  ( 112.1359432235843059, 200.5768536076146233, -142.3325995572699298 ) ) ;
#25735=DIRECTION ( 'NONE',  ( 0.000000000000000000, 0.000000000000000000, -1.000000000000000000 ) ) ;
#25737=CARTESIAN_POINT ( 'NONE',  ( 161.3687566780243685, 205.6878092301651009, -150.9609010065648818 ) ) ;
#25741=FACE_BOUND ( 'NONE', #16491, .T. ) ;
#25767=DIRECTION ( 'NONE',  ( 0.000000000000000000, 0.000000000000000000, -1.000000000000000000 ) ) ;
#25777=CARTESIAN_POINT ( 'NONE',  ( 155.2453482286826727, 220.0000000000000284, -189.9999999999999716 ) ) ;
#25793=SPHERICAL_SURFACE ( 'NONE', #28114, 35.18636678425505693 ) ;
#25798=AXIS2_PLACEMENT_3D ( 'NONE', #14908, #1676, #28092 ) ;
#25822=CIRCLE ( 'NONE', #10673, 17.93072811908088937 ) ;
#25923=DIRECTION ( 'NONE',  ( -0.000000000000000000, -1.000000000000000000, -0.000000000000000000 ) ) ;
#25931=FACE_OUTER_BOUND ( 'NONE', #5731, .T. ) ;
#25958=CARTESIAN_POINT ( 'NONE',  ( 129.0397224731839287, 249.4020613294620148, -144.2074248490017396 ) ) ;
#25963=SPHERICAL_SURFACE ( 'NONE', #18959, 35.18636678425505693 ) ;
#25976=ORIENTED_EDGE ( 'NONE', *, *, #23762, .F. ) ;
#25980=CARTESIAN_POINT ( 'NONE',  ( 134.9999999999998579, 404.6636166603179277, -152.9999999999999716 ) ) ;
#25981=EDGE_CURVE ( 'NONE', #23466, #24318, #13639, .T. ) ;
#26018=CARTESIAN_POINT ( 'NONE',  ( 160.9807621135329612, 204.9999999999999147, -138.9999999999999432 ) ) ;
#26032=CARTESIAN_POINT ( 'NONE',  ( 134.9999999999998579, 433.5940952139197293, -145.0000000000000000 ) ) ;
#26053=DIRECTION ( 'NONE',  ( 0.000000000000000000, 0.000000000000000000, -1.000000000000000000 ) ) ;
#26060=DIRECTION ( 'NONE',  ( 0.8660254037844432595, 0.4999999999999919509, -0.000000000000000000 ) ) ;
#26102=DIRECTION ( 'NONE',  ( 0.000000000000000000, 0.000000000000000000, 1.000000000000000000 ) ) ;
#26104=CARTESIAN_POINT ( 'NONE',  ( 106.8096100835816458, 209.7359181041861689, -148.0084258618598199 ) ) ;
#26134=CARTESIAN_POINT ( 'NONE',  ( 109.2179431711400639, 204.6558323512134621, -151.0000000000000853 ) ) ;
#26184=FACE_OUTER_BOUND ( 'NONE', #13742, .T. ) ;
#26242=DIRECTION ( 'NONE',  ( -1.000000000000000000, 0.000000000000000000, 0.000000000000000000 ) ) ;
#26248=CARTESIAN_POINT ( 'NONE',  ( 134.9999999999998579, 220.0000000000000284, -169.9999999999999716 ) ) ;
#26249=ADVANCED_FACE ( 'NONE', ( #26184 ), #46, .T. ) ;
#26262=ORIENTED_EDGE ( 'NONE', *, *, #9711, .T. ) ;
#26265=CARTESIAN_POINT ( 'NONE',  ( 349.0018770490532916, 96.44595867864242678, -134.2811822434183853 ) ) ;
#26267=TOROIDAL_SURFACE ( 'NONE', #25798, 7.509856658345970715, 10.53396790234564762 ) ;
#26272=DIRECTION ( 'NONE',  ( -0.000000000000000000, -1.000000000000000000, -0.000000000000000000 ) ) ;
#26295=VERTEX_POINT ( 'NONE', #23900 ) ;
#26299=ORIENTED_EDGE ( 'NONE', *, *, #8328, .F. ) ;
#26303=CARTESIAN_POINT ( 'NONE',  ( 158.2674871941218839, 201.0613226313178075, -148.6640466283485580 ) ) ;
#26335=DIRECTION ( 'NONE',  ( -1.000000000000000000, 0.000000000000000000, 0.000000000000000000 ) ) ;
#26360=ORIENTED_EDGE ( 'NONE', *, *, #12, .T. ) ;
#26378=ORIENTED_EDGE ( 'NONE', *, *, #14530, .T. ) ;
#26427=ORIENTED_EDGE ( 'NONE', *, *, #6752, .T. ) ;
#26437=CARTESIAN_POINT ( 'NONE',  ( 158.9573448901061852, 201.9403141824000443, -140.2307156351394610 ) ) ;
#26461=EDGE_CURVE ( 'NONE', #3815, #28048, #12286, .T. ) ;
#26482=CARTESIAN_POINT ( 'NONE',  ( 140.8457514438942155, 249.4249679671852107, -146.3660979730027520 ) ) ;
#26485=( LENGTH_UNIT ( ) NAMED_UNIT ( * ) SI_UNIT ( .MILLI., .METRE. ) );
#26521=CARTESIAN_POINT ( 'NONE',  ( 107.7914849032574551, 207.3616777871659167, -139.6178255645964441 ) ) ;
#26537=AXIS2_PLACEMENT_3D ( 'NONE', #17165, #25923, #23773 ) ;
#26583=CARTESIAN_POINT ( 'NONE',  ( 160.7828204114136952, 204.6609985789451969, -139.0095862629495116 ) ) ;
#26599=EDGE_CURVE ( 'NONE', #13520, #15076, #12733, .T. ) ;
#26613=CARTESIAN_POINT ( 'NONE',  ( 338.9795809418241106, 102.2323340340494724, -145.0000000000000000 ) ) ;
#26633=CARTESIAN_POINT ( 'NONE',  ( 139.5211538318895066, 249.6587006023211188, -141.0358260266775687 ) ) ;
#26641=ORIENTED_EDGE ( 'NONE', *, *, #15621, .F. ) ;
#26658=DIRECTION ( 'NONE',  ( -0.000000000000000000, -1.000000000000000000, -0.000000000000000000 ) ) ;
#26741=VERTEX_POINT ( 'NONE', #24722 ) ;
#26788=CARTESIAN_POINT ( 'NONE',  ( 137.6591494508433300, 249.8824263794485319, -139.6178255645964725 ) ) ;
#26816=AXIS2_PLACEMENT_3D ( 'NONE', #26248, #13196, #18212 ) ;
#26821=SPHERICAL_SURFACE ( 'NONE', #17463, 35.18636678425505693 ) ;
#26831=ORIENTED_EDGE ( 'NONE', *, *, #23822, .F. ) ;
#26848=CARTESIAN_POINT ( 'NONE',  ( 294.9233831825460470, 127.6681916698403114, -153.0000000000000000 ) ) ;
#26897=CIRCLE ( 'NONE', #286, 7.999999999999979572 ) ;
#26902=ORIENTED_EDGE ( 'NONE', *, *, #20263, .T. ) ;
#26908=AXIS2_PLACEMENT_3D ( 'NONE', #22917, #22780, #9567 ) ;
#26920=DIRECTION ( 'NONE',  ( 0.000000000000000000, 0.000000000000000000, -1.000000000000000000 ) ) ;
#26931=CARTESIAN_POINT ( 'NONE',  ( 136.9357406746122479, 249.9396928751734492, -139.3072807822095740 ) ) ;
#26939=EDGE_LOOP ( 'NONE', ( #12572, #13416, #10265, #14027 ) ) ;
#27008=VERTEX_POINT ( 'NONE', #25980 ) ;
#27026=DIRECTION ( 'NONE',  ( -0.8660254037844362651, 0.5000000000000039968, -0.000000000000000000 ) ) ;
#27077=EDGE_LOOP ( 'NONE', ( #21985, #2952, #21345, #27413 ) ) ;
#27192=AXIS2_PLACEMENT_3D ( 'NONE', #16635, #16221, #25246 ) ;
#27194=CARTESIAN_POINT ( 'NONE',  ( 162.6191355986925373, 208.2828629619915830, -140.2311020877163799 ) ) ;
#27257=FACE_OUTER_BOUND ( 'NONE', #20824, .T. ) ;
#27282=EDGE_LOOP ( 'NONE', ( #27688, #13303, #22978, #6759 ) ) ;
#27286=AXIS2_PLACEMENT_3D ( 'NONE', #20411, #7629, #875 ) ;
#27293=CARTESIAN_POINT ( 'NONE',  ( 112.3374974218580320, 200.3420669299287340, -146.9347961558894156 ) ) ;
#27333=ORIENTED_EDGE ( 'NONE', *, *, #8385, .T. ) ;
#27364=FACE_OUTER_BOUND ( 'NONE', #21526, .T. ) ;
#27413=ORIENTED_EDGE ( 'NONE', *, *, #3228, .T. ) ;
#27434=AXIS2_PLACEMENT_3D ( 'NONE', #18618, #1513, #20913 ) ;
#27523=FACE_OUTER_BOUND ( 'NONE', #23126, .T. ) ;
#27532=CIRCLE ( 'NONE', #2770, 10.00000000000000888 ) ;
#27534=CARTESIAN_POINT ( 'NONE',  ( 130.4830771568834962, 249.6593242776497164, -141.0313312019551688 ) ) ;
#27550=ORIENTED_EDGE ( 'NONE', *, *, #11443, .T. ) ;
#27552=B_SPLINE_CURVE_WITH_KNOTS ( 'NONE', 3,
 ( #7735, #709, #16505, #14627, #27677, #23811, #3839, #4118, #27816, #14916, #12762, #27534, #3975, #17199, #21503, #12626, #25533, #1403, #10313, #25958, #21650, #1820, #16916, #7872, #23246, #5852, #8154, #21364, #3550, #10595, #6278, #19071, #19352, #12904, #12483, #23381, #1962, #17056, #28099, #21082, #8014, #8443 ),
 .UNSPECIFIED., .F., .F.,
 ( 4, 2, 2, 2, 2, 2, 2, 2, 2, 2, 2, 2, 2, 2, 2, 2, 2, 2, 2, 2, 4 ),
 ( 0.01880622955133632798, 0.01998131524074754292, 0.02115640093015875439, 0.02174394377486431329, 0.02233148661956986872, 0.02350657230898093447, 0.02468165799839200023, 0.02585674368780306598, 0.02644428653250857630, 0.02703182937721408663, 0.02820691506662520442, 0.02938200075603631875, 0.03055708644544743655, 0.03173217213485855087, 0.03231971497956409589, 0.03290725782426963397, 0.03408234351368061299, 0.03525742920309159201, 0.03584497204779707458, 0.03643251489250255715, 0.03760760058191346678 ),
 .UNSPECIFIED. ) ;
#27646=DIRECTION ( 'NONE',  ( -0.4999999999999919509, 0.8660254037844432595, -1.224646799147353207E-16 ) ) ;
#27666=DIRECTION ( 'NONE',  ( -0.000000000000000000, -1.000000000000000000, -0.000000000000000000 ) ) ;
#27677=CARTESIAN_POINT ( 'NONE',  ( 133.0634450963849531, 249.9396218376480192, -139.3076717160242879 ) ) ;
#27682=DIRECTION ( 'NONE',  ( -0.7071067811865489050, 0.000000000000000000, -0.7071067811865462405 ) ) ;
#27686=CARTESIAN_POINT ( 'NONE',  ( 107.0548155441414195, 209.0846731383313966, -148.9655004847909936 ) ) ;
#27688=ORIENTED_EDGE ( 'NONE', *, *, #5394, .F. ) ;
#27709=CARTESIAN_POINT ( 'NONE',  ( 111.5727331380326319, 201.2585679321024088, -141.0313312019552541 ) ) ;
#27789=DIRECTION ( 'NONE',  ( 0.8660254037844432595, 0.4999999999999919509, -0.000000000000000000 ) ) ;
#27802=TOROIDAL_SURFACE ( 'NONE', #15443, 7.509856658345970715, 10.53396790234564762 ) ;
#27816=CARTESIAN_POINT ( 'NONE',  ( 131.8275543060484267, 249.8322405497061993, -139.9035143180224736 ) ) ;
#27822=ORIENTED_EDGE ( 'NONE', *, *, #14581, .F. ) ;
#27826=DIRECTION ( 'NONE',  ( 0.000000000000000000, 0.000000000000000000, 1.000000000000000000 ) ) ;
#27908=DIRECTION ( 'NONE',  ( -0.000000000000000000, -1.000000000000000000, -0.000000000000000000 ) ) ;
#27913=DIRECTION ( 'NONE',  ( 0.000000000000000000, 0.000000000000000000, -1.000000000000000000 ) ) ;
#27959=DIRECTION ( 'NONE',  ( 1.000000000000000000, 0.000000000000000000, 0.000000000000000000 ) ) ;
#27960=EDGE_LOOP ( 'NONE', ( #370, #6289 ) ) ;
#27966=CARTESIAN_POINT ( 'NONE',  ( 108.0238497313615227, 206.8729107250730408, -150.6165463336312769 ) ) ;
#27968=ORIENTED_EDGE ( 'NONE', *, *, #22133, .T. ) ;
#28048=VERTEX_POINT ( 'NONE', #21772 ) ;
#28049=CIRCLE ( 'NONE', #16148, 17.93072811908088937 ) ;
#28058=CYLINDRICAL_SURFACE ( 'NONE', #3456, 10.00000000000000888 ) ;
#28080=CARTESIAN_POINT ( 'NONE',  ( -49.97791255360778706, 113.2029523930418975, -145.0000000000000000 ) ) ;
#28092=DIRECTION ( 'NONE',  ( 0.000000000000000000, 0.000000000000000000, -1.000000000000000000 ) ) ;
#28099=CARTESIAN_POINT ( 'NONE',  ( 133.6295840780252036, 249.9693091936576081, -150.8447356795924179 ) ) ;
#28114=AXIS2_PLACEMENT_3D ( 'NONE', #6121, #13030, #12462 ) ;
#28167=CARTESIAN_POINT ( 'NONE',  ( 160.1668614390261496, 203.6666592782660246, -139.1934629298939683 ) ) ;
#28190=ORIENTED_EDGE ( 'NONE', *, *, #8328, .T. ) ;
#28229=AXIS2_PLACEMENT_3D ( 'NONE', #17720, #2196, #26335 ) ;
#28253=CARTESIAN_POINT ( 'NONE',  ( 106.6102839382104719, 210.3032261119582813, -146.5591841905930721 ) ) ;
#28258=EDGE_LOOP ( 'NONE', ( #14398, #20352, #26262, #20579 ) ) ;
#28280=VERTEX_POINT ( 'NONE', #22632 ) ;
#28290=ORIENTED_EDGE ( 'NONE', *, *, #15132, .T. ) ;
#28302=DIRECTION ( 'NONE',  ( -0.000000000000000000, 0.000000000000000000, 1.000000000000000000 ) ) ;
#28338=CARTESIAN_POINT ( 'NONE',  ( 134.9999999999998579, 220.0000000000000284, 109.9999999999999858 ) ) ;
#28352=AXIS2_PLACEMENT_3D ( 'NONE', #1375, #12170, #16884 ) ;
#28382=DIRECTION ( 'NONE',  ( 0.000000000000000000, 0.000000000000000000, -1.000000000000000000 ) ) ;
#28442=COLOUR_RGB('Black',0.12,0.14,0.17);
#28443=FILL_AREA_STYLE_COLOUR('',#28442);
#28444=FILL_AREA_STYLE('',(#28443));
#28445=SURFACE_STYLE_FILL_AREA(#28444);
#28446=SURFACE_SIDE_STYLE('',(#28445));
#28447=SURFACE_STYLE_USAGE(.BOTH.,#28446);
#28448=PRESENTATION_STYLE_ASSIGNMENT((#28447));
ENDSEC;
END-ISO-10303-21;
